ISO-10303-21;
HEADER;
FILE_DESCRIPTION (('STEP AP214'),
    '1' );
FILE_NAME ('hex flange nut gradea_iso_ISO - 4161 - M5 - N.step',
    '2026-10-24T07:08:27',
    ( '' ),
    ( '' ),
    'SwSTEP 2.0',
    'SolidWorks 2026',
    '' );
FILE_SCHEMA (( 'AUTOMOTIVE_DESIGN' ));
ENDSEC;

DATA;
#1=CARTESIAN_POINT ( 'NONE',  ( 0.000000000000000000, 0.000000000000000000, 0.000000000000000000 ) ) ;
#63=SURFACE_STYLE_USAGE ( .BOTH. , #18719 ) ;
#65=B_SPLINE_CURVE_WITH_KNOTS ( 'NONE', 3,
 ( #1226, #12839, #18639, #3001, #8800, #7452 ),
 .UNSPECIFIED., .F., .F.,
 ( 4, 2, 4 ),
 ( 0.002365888236227977302, 0.003551327329835078910, 0.004736766423442180518 ),
 .UNSPECIFIED. ) ;
#76=UNCERTAINTY_MEASURE_WITH_UNIT (LENGTH_MEASURE( 1.000000000000000082E-05 ), #4261, 'distance_accuracy_value', 'NONE');
#104=VERTEX_POINT ( 'NONE', #18489 ) ;
#119=DIRECTION ( 'NONE',  ( -0.000000000000000000, -0.000000000000000000, 1.000000000000000000 ) ) ;
#121=CARTESIAN_POINT ( 'NONE',  ( 0.000000000000000000, 0.000000000000000000, 3.469446951953614189E-15 ) ) ;
#124=DIRECTION ( 'NONE',  ( -0.000000000000000000, -0.000000000000000000, 1.000000000000000000 ) ) ;
#127=CARTESIAN_POINT ( 'NONE',  ( -4.211140560182196957, 2.431303136016537803, -3.745885042887433514 ) ) ;
#132=CARTESIAN_POINT ( 'NONE',  ( 2.000000000000008882, 3.464101615137749945, 0.000000000000000000 ) ) ;
#157=CARTESIAN_POINT ( 'NONE',  ( 2.000000000000008882, 3.464101615137749945, 0.000000000000000000 ) ) ;
#163=EDGE_LOOP ( 'NONE', ( #2540, #2042, #15896, #16236 ) ) ;
#185=AXIS2_PLACEMENT_3D ( 'NONE', #9363, #1260, #1164 ) ;
#187=CARTESIAN_POINT ( 'NONE',  ( -4.211399284164270895, 2.459729995988205964, -3.751162237960538715 ) ) ;
#230=CARTESIAN_POINT ( 'NONE',  ( 2.499999999999999556, 0.000000000000000000, 3.469446951953614189E-15 ) ) ;
#251=CARTESIAN_POINT ( 'NONE',  ( 2.000000000000005329, -3.464101615137751722, 0.000000000000000000 ) ) ;
#266=CIRCLE ( 'NONE', #8445, 2.500000000000000444 ) ;
#281=CARTESIAN_POINT ( 'NONE',  ( -4.197477534772231955, 0.8522413273724368521, -3.505042416683225692 ) ) ;
#290=ORIENTED_EDGE ( 'NONE', *, *, #8143, .F. ) ;
#302=CARTESIAN_POINT ( 'NONE',  ( -1.149515148933662080E-15, -4.736529461166056443, -3.681130640444383317 ) ) ;
#328=CARTESIAN_POINT ( 'NONE',  ( -4.000000000000000000, -2.309401076758512694, -3.433295621305382461 ) ) ;
#352=CARTESIAN_POINT ( 'NONE',  ( -1.360585162435467455, 4.061296242128285883, -3.505054077164959203 ) ) ;
#358=CARTESIAN_POINT ( 'NONE',  ( -4.000000000000000000, 2.309401076758498483, -3.433295621305379353 ) ) ;
#387=CARTESIAN_POINT ( 'NONE',  ( -6.473970235329672780E-16, -4.862606272033106691, -3.745885042887442395 ) ) ;
#399=DIRECTION ( 'NONE',  ( -1.000000000000000000, 0.000000000000000000, 0.000000000000000000 ) ) ;
#415=CARTESIAN_POINT ( 'NONE',  ( -4.000000000000000888, -1.539600717839011201, -3.300726591567081591 ) ) ;
#427=EDGE_CURVE ( 'NONE', #12688, #15321, #15425, .T. ) ;
#440=CARTESIAN_POINT ( 'NONE',  ( 0.1404048886732821022, 4.699864953788070565, -3.686887068327037387 ) ) ;
#441=ORIENTED_EDGE ( 'NONE', *, *, #15622, .T. ) ;
#472=B_SPLINE_CURVE_WITH_KNOTS ( 'NONE', 3,
 ( #4129, #15648, #2699, #8507, #14321, #1186, #18795, #1365 ),
 .UNSPECIFIED., .F., .F.,
 ( 4, 2, 2, 4 ),
 ( 0.005725059856848641743, 0.006314084072593626612, 0.006903108288338611481, 0.008081156719828581220 ),
 .UNSPECIFIED. ) ;
#525=CARTESIAN_POINT ( 'NONE',  ( -2.805705207896067144, 3.226868319750155312, -3.503898532754364581 ) ) ;
#544=CARTESIAN_POINT ( 'NONE',  ( -2.807080416178626692, 3.225969019225154444, -3.502507215260441065 ) ) ;
#552=CARTESIAN_POINT ( 'NONE',  ( 4.236525694536557474, -2.416953475386482530, -3.751298745799839462 ) ) ;
#577=CIRCLE ( 'NONE', #3336, 5.560781378645573980 ) ;
#582=CARTESIAN_POINT ( 'NONE',  ( 4.211399257449709665, -2.459727064652517114, -3.751161691472417736 ) ) ;
#611=CARTESIAN_POINT ( 'NONE',  ( -4.197393957002303999, -7.773935952363655451E-14, -3.503767560748929810 ) ) ;
#626=LINE ( 'NONE', #18240, #10043 ) ;
#673=CARTESIAN_POINT ( 'NONE',  ( 3.999999999999998224, 2.472263674411418588, -3.687027874309861897 ) ) ;
#678=CARTESIAN_POINT ( 'NONE',  ( 0.000000000000000000, 0.000000000000000000, -4.974599999999998801 ) ) ;
#714=EDGE_CURVE ( 'NONE', #10711, #18131, #266, .T. ) ;
#780=EDGE_CURVE ( 'NONE', #16201, #10824, #11466, .T. ) ;
#781=CARTESIAN_POINT ( 'NONE',  ( -4.000000000000000000, -0.3979232138631226823, -3.896351557369779711E-17 ) ) ;
#784=CONICAL_SURFACE ( 'NONE', #835, 2.500000000000000888, 0.9599310885968785900 ) ;
#787=AXIS2_PLACEMENT_3D ( 'NONE', #12286, #18289, #16680 ) ;
#791=FACE_OUTER_BOUND ( 'NONE', #14669, .T. ) ;
#802=B_SPLINE_CURVE_WITH_KNOTS ( 'NONE', 3,
 ( #3372, #6127, #1400, #7646, #7204 ),
 .UNSPECIFIED., .F., .F.,
 ( 4, 1, 4 ),
 ( 0.000000000000000000, 0.002309401076758505356, 0.004618802153517010713 ),
 .UNSPECIFIED. ) ;
#820=AXIS2_PLACEMENT_3D ( 'NONE', #962, #5232, #12193 ) ;
#825=ORIENTED_EDGE ( 'NONE', *, *, #3033, .T. ) ;
#835=AXIS2_PLACEMENT_3D ( 'NONE', #1508, #11788, #18648 ) ;
#839=CARTESIAN_POINT ( 'NONE',  ( -2.500000000000000888, 0.000000000000000000, -4.974599999999998801 ) ) ;
#900=CARTESIAN_POINT ( 'NONE',  ( 0.000000000000000000, 0.000000000000000000, -4.974599999999998801 ) ) ;
#922=CARTESIAN_POINT ( 'NONE',  ( 4.000000000000000000, 2.309401076758497151, -3.433295621305379353 ) ) ;
#926=CARTESIAN_POINT ( 'NONE',  ( 0.6448876103708359731, 4.246476118072354922, -0.2256878752776725616 ) ) ;
#945=CARTESIAN_POINT ( 'NONE',  ( 4.175002511812151873, 2.208363329454889445, -3.469254087858244073 ) ) ;
#961=CARTESIAN_POINT ( 'NONE',  ( 4.000000000000000000, -2.309401076758516691, -0.4999999999999995559 ) ) ;
#962=CARTESIAN_POINT ( 'NONE',  ( 8.673617379884035472E-16, 4.618802153517012954, -5.000000000000000000 ) ) ;
#964=EDGE_CURVE ( 'NONE', #15321, #11704, #17262, .T. ) ;
#988=ADVANCED_FACE ( 'NONE', ( #14004, #12479 ), #3723, .T. ) ;
#999=ORIENTED_EDGE ( 'NONE', *, *, #11126, .T. ) ;
#1002=CARTESIAN_POINT ( 'NONE',  ( -3.349226789952655547, -2.685125164760744809, -0.2236248678334863682 ) ) ;
#1016=CARTESIAN_POINT ( 'NONE',  ( 0.000000000000000000, 0.000000000000000000, -5.000000000000000000 ) ) ;
#1031=CARTESIAN_POINT ( 'NONE',  ( -0.02511973781850462134, 4.877415612947412882, -3.751298745799839462 ) ) ;
#1034=ORIENTED_EDGE ( 'NONE', *, *, #13070, .T. ) ;
#1073=DIRECTION ( 'NONE',  ( -1.000000000000000000, 0.000000000000000000, 0.000000000000000000 ) ) ;
#1086=EDGE_LOOP ( 'NONE', ( #17308, #8677, #4999, #18206 ) ) ;
#1092=AXIS2_PLACEMENT_3D ( 'NONE', #3107, #3481, #15008 ) ;
#1096=ADVANCED_FACE ( 'NONE', ( #13912 ), #13894, .T. ) ;
#1115=APPLICATION_CONTEXT ( 'automotive_design' ) ;
#1155=CARTESIAN_POINT ( 'NONE',  ( -1.391697335622809950, -4.043246145443391448, -3.503898532754372575 ) ) ;
#1160=CONICAL_SURFACE ( 'NONE', #12711, 4.000000000000000000, 0.8911886515913786111 ) ;
#1164=DIRECTION ( 'NONE',  ( -1.000000000000000000, 0.000000000000000000, 0.000000000000000000 ) ) ;
#1186=CARTESIAN_POINT ( 'NONE',  ( -4.000000000000000888, 1.563622288139195238, -0.2253451193528307472 ) ) ;
#1188=FACE_OUTER_BOUND ( 'NONE', #17037, .T. ) ;
#1190=DIRECTION ( 'NONE',  ( -0.5000000000000016653, 0.8660254037844378194, 0.000000000000000000 ) ) ;
#1193=DIRECTION ( 'NONE',  ( 0.000000000000000000, 0.000000000000000000, -1.000000000000000000 ) ) ;
#1197=CARTESIAN_POINT ( 'NONE',  ( 0.000000000000000000, 0.000000000000000000, 0.000000000000000000 ) ) ;
#1226=CARTESIAN_POINT ( 'NONE',  ( -2.000000000000006661, 3.464101615137750834, 0.000000000000000000 ) ) ;
#1255=DIRECTION ( 'NONE',  ( -0.000000000000000000, -0.000000000000000000, 1.000000000000000000 ) ) ;
#1260=DIRECTION ( 'NONE',  ( -0.000000000000000000, 0.000000000000000000, -1.000000000000000000 ) ) ;
#1263=ADVANCED_FACE ( 'NONE', ( #18264 ), #18579, .F. ) ;
#1285=ORIENTED_EDGE ( 'NONE', *, *, #6025, .T. ) ;
#1330=EDGE_CURVE ( 'NONE', #5282, #4170, #6921, .T. ) ;
#1334=EDGE_CURVE ( 'NONE', #11781, #17591, #6650, .T. ) ;
#1337=CARTESIAN_POINT ( 'NONE',  ( -3.861362476283256129, -2.629030857716004199, -3.671615880910374941 ) ) ;
#1353=VERTEX_POINT ( 'NONE', #230 ) ;
#1365=CARTESIAN_POINT ( 'NONE',  ( -4.000000000000000000, 2.309401076758498483, -0.4999999999999927280 ) ) ;
#1378=CARTESIAN_POINT ( 'NONE',  ( 0.000000000000000000, 0.000000000000000000, -5.000000000000000000 ) ) ;
#1400=CARTESIAN_POINT ( 'NONE',  ( 2.000000000000000444, 3.464101615137754830, -3.142992957459231018 ) ) ;
#1404=AXIS2_PLACEMENT_3D ( 'NONE', #15196, #16895, #9551 ) ;
#1407=TOROIDAL_SURFACE ( 'NONE', #6865, 5.384454397937118664, 0.5155456020628804703 ) ;
#1411=CARTESIAN_POINT ( 'NONE',  ( -4.024497503033714452, -2.323544716729502468, -3.572167766733752803 ) ) ;
#1422=CARTESIAN_POINT ( 'NONE',  ( -4.211140560182196957, 2.431303136016537803, -3.745885042887433514 ) ) ;
#1425=CARTESIAN_POINT ( 'NONE',  ( -4.204114297095464359, 1.660363174096617156, -3.602136431857887011 ) ) ;
#1442=AXIS2_PLACEMENT_3D ( 'NONE', #14267, #11299, #17126 ) ;
#1454=DIRECTION ( 'NONE',  ( -0.000000000000000000, -0.000000000000000000, 1.000000000000000000 ) ) ;
#1461=EDGE_CURVE ( 'NONE', #4891, #11483, #65, .T. ) ;
#1495=DIRECTION ( 'NONE',  ( 0.8660254037844374864, -0.5000000000000018874, 0.000000000000000000 ) ) ;
#1503=CARTESIAN_POINT ( 'NONE',  ( 4.000000000000000000, -2.309401076758514915, -3.433295621305383349 ) ) ;
#1504=LINE ( 'NONE', #4443, #15007 ) ;
#1508=CARTESIAN_POINT ( 'NONE',  ( 0.000000000000000000, 0.000000000000000000, -4.974599999999998801 ) ) ;
#1521=EDGE_LOOP ( 'NONE', ( #1285, #15685, #17663, #2177 ) ) ;
#1562=CARTESIAN_POINT ( 'NONE',  ( -2.500000000000000444, 3.061616997868383634E-16, -5.000000000000000888 ) ) ;
#1570=FACE_OUTER_BOUND ( 'NONE', #1521, .T. ) ;
#1594=FACE_OUTER_BOUND ( 'NONE', #1870, .T. ) ;
#1631=ORIENTED_EDGE ( 'NONE', *, *, #10360, .T. ) ;
#1643=B_SPLINE_CURVE_WITH_KNOTS ( 'NONE', 3,
 ( #4932, #9027, #7780, #1798 ),
 .UNSPECIFIED., .F., .F.,
 ( 4, 4 ),
 ( 0.000000000000000000, 0.002452478801916376308 ),
 .UNSPECIFIED. ) ;
#1649=( BOUNDED_SURFACE ( )  B_SPLINE_SURFACE ( 3, 2, ( 
 ( #10852, #3639, #8002 ),
 ( #12486, #18291, #13813 ),
 ( #12388, #14387, #14470 ),
 ( #17074, #17350, #9816 ),
 ( #18672, #16970, #15628 ),
 ( #11142, #9906, #12958 ) ),
 .UNSPECIFIED., .F., .F., .F. ) 
 B_SPLINE_SURFACE_WITH_KNOTS ( ( 4, 2, 4 ),
 ( 3, 3 ),
 ( 0.02032853247518126918, 0.02278863295364821906, 0.02524873343211516893 ),
 ( 0.000000000000000000, 1.000000000000000000 ),
 .UNSPECIFIED. ) 
 GEOMETRIC_REPRESENTATION_ITEM ( )  RATIONAL_B_SPLINE_SURFACE ( (
 ( 1.000000000000000000, 0.8047781615896838492, 1.000000000000000000),
 ( 1.000000000000000000, 0.8123767586288186404, 1.000000000000000000),
 ( 1.000000000000000000, 0.8190662415565814758, 1.000000000000000000),
 ( 1.000000000000000000, 0.8192361015667604107, 1.000000000000000000),
 ( 1.000000000000000000, 0.8126135807104967190, 1.000000000000000000),
 ( 1.000000000000000000, 0.8047712338318580017, 1.000000000000000000) ) ) 
 REPRESENTATION_ITEM ( '' )  SURFACE ( )  );
#1667=CARTESIAN_POINT ( 'NONE',  ( 1.257172072275274388, -3.892973519170983110, -3.433252694550781303 ) ) ;
#1686=AXIS2_PLACEMENT_3D ( 'NONE', #5238, #13727, #9149 ) ;
#1697=CARTESIAN_POINT ( 'NONE',  ( -4.000000000000000000, 0.8730739991738342143, -3.223134629628428893 ) ) ;
#1728=CARTESIAN_POINT ( 'NONE',  ( -3.333333333333335258, 2.694301256218251783, -3.300726591567079815 ) ) ;
#1750=CARTESIAN_POINT ( 'NONE',  ( 1.391697335622810172, 4.043246145443375461, -3.503898532754365913 ) ) ;
#1766=ORIENTED_EDGE ( 'NONE', *, *, #9354, .T. ) ;
#1769=VECTOR ( 'NONE', #6486, 1000.000000000000227 ) ;
#1798=CARTESIAN_POINT ( 'NONE',  ( -4.197393957002303999, -7.773935952363655451E-14, -3.503767560748929810 ) ) ;
#1799=ORIENTED_EDGE ( 'NONE', *, *, #964, .F. ) ;
#1832=ORIENTED_EDGE ( 'NONE', *, *, #7124, .T. ) ;
#1858=CARTESIAN_POINT ( 'NONE',  ( -0.1750025118121544265, -4.719839900820635314, -3.469254087858253399 ) ) ;
#1870=EDGE_LOOP ( 'NONE', ( #9986, #7665, #15841, #9983 ) ) ;
#1876=CONICAL_SURFACE ( 'NONE', #17394, 4.000000000000000000, 0.8911886515913786111 ) ;
#1889=ORIENTED_EDGE ( 'NONE', *, *, #8091, .F. ) ;
#1892=CIRCLE ( 'NONE', #13151, 4.000000000000000000 ) ;
#1902=CARTESIAN_POINT ( 'NONE',  ( -4.000000000000000000, -2.309401076758512694, -3.433295621305382461 ) ) ;
#1905=VERTEX_POINT ( 'NONE', #10025 ) ;
#1928=LINE ( 'NONE', #8882, #14841 ) ;
#1935=CARTESIAN_POINT ( 'NONE',  ( 3.333333333333335702, -2.694301256218268215, -3.300726591567084256 ) ) ;
#1947=FACE_BOUND ( 'NONE', #2837, .T. ) ;
#1951=CARTESIAN_POINT ( 'NONE',  ( 3.679171394226031122, 2.494631558665830973, -0.3503314178412474389 ) ) ;
#1959=CARTESIAN_POINT ( 'NONE',  ( -0.6640947660597427138, 4.471078309994878985, -3.602146406945963442 ) ) ;
#2036=AXIS2_PLACEMENT_3D ( 'NONE', #7128, #15817, #2670 ) ;
#2042=ORIENTED_EDGE ( 'NONE', *, *, #16122, .F. ) ;
#2088=CARTESIAN_POINT ( 'NONE',  ( 3.680118525130245732, -2.494084732383344605, -0.3507732604232533524 ) ) ;
#2104=CARTESIAN_POINT ( 'NONE',  ( 0.000000000000000000, 0.000000000000000000, -4.694516984716113228 ) ) ;
#2136=CARTESIAN_POINT ( 'NONE',  ( -4.211140560182196957, 2.431303136016537803, -3.745885042887433514 ) ) ;
#2148=CARTESIAN_POINT ( 'NONE',  ( 0.000000000000000000, 0.000000000000000000, 0.000000000000000000 ) ) ;
#2155=DIRECTION ( 'NONE',  ( 0.000000000000000000, 0.000000000000000000, -1.000000000000000000 ) ) ;
#2177=ORIENTED_EDGE ( 'NONE', *, *, #12687, .F. ) ;
#2180=ORIENTED_EDGE ( 'NONE', *, *, #11126, .F. ) ;
#2189=CARTESIAN_POINT ( 'NONE',  ( 3.999999999999999112, -0.7890432684750902093, -0.04868663549882291247 ) ) ;
#2190=DIRECTION ( 'NONE',  ( 1.000000000000000000, 0.000000000000000000, 0.000000000000000000 ) ) ;
#2196=FACE_OUTER_BOUND ( 'NONE', #163, .T. ) ;
#2219=LINE ( 'NONE', #14037, #16226 ) ;
#2239=ADVANCED_FACE ( 'NONE', ( #11041 ), #16863, .F. ) ;
#2257=CARTESIAN_POINT ( 'NONE',  ( 2.742827927723449299, 3.035229711104609596, -3.433252694550591233 ) ) ;
#2269=VERTEX_POINT ( 'NONE', #4471 ) ;
#2278=CARTESIAN_POINT ( 'NONE',  ( 4.204115023516791005, -1.660442669500199919, -3.602151381774560068 ) ) ;
#2295=CIRCLE ( 'NONE', #787, 0.5155456020628804703 ) ;
#2341=CONICAL_SURFACE ( 'NONE', #5085, 2.059999999999998721, 0.9599310885968738161 ) ;
#2355=ORIENTED_EDGE ( 'NONE', *, *, #7952, .F. ) ;
#2367=VERTEX_POINT ( 'NONE', #2672 ) ;
#2384=CARTESIAN_POINT ( 'NONE',  ( -4.000000000000000000, 2.511478553582031203, -3.469254451724764543 ) ) ;
#2387=DIRECTION ( 'NONE',  ( 0.000000000000000000, 0.000000000000000000, 1.000000000000000000 ) ) ;
#2417=ORIENTED_EDGE ( 'NONE', *, *, #11097, .F. ) ;
#2423=CARTESIAN_POINT ( 'NONE',  ( -3.679171394226034675, -2.494631558665844739, -0.3503314178412558211 ) ) ;
#2432=EDGE_CURVE ( 'NONE', #1905, #16921, #7302, .T. ) ;
#2473=CARTESIAN_POINT ( 'NONE',  ( 4.197310751797292738, 0.8178363989516252985, -3.502498386812444409 ) ) ;
#2517=SHAPE_REPRESENTATION ( 'hex flange nut gradea_iso_ISO - 4161 - M5 - N', ( #8017 ), #6229 ) ;
#2540=ORIENTED_EDGE ( 'NONE', *, *, #8625, .F. ) ;
#2548=AXIS2_PLACEMENT_3D ( 'NONE', #18401, #11647, #12898 ) ;
#2565=CARTESIAN_POINT ( 'NONE',  ( 1.734723475976807094E-15, 4.618802153517012954, -0.4999999999999995559 ) ) ;
#2632=VECTOR ( 'NONE', #119, 1000.000000000000000 ) ;
#2648=CIRCLE ( 'NONE', #12683, 2.100000000000000089 ) ;
#2669=CARTESIAN_POINT ( 'NONE',  ( -2.804994570502171047, -3.229033611042465335, -3.526374918436838701 ) ) ;
#2670=DIRECTION ( 'NONE',  ( 1.000000000000000000, 0.000000000000000000, 0.000000000000000000 ) ) ;
#2672=CARTESIAN_POINT ( 'NONE',  ( 2.500000000000000888, 3.061616997868384127E-16, -4.974599999999998801 ) ) ;
#2699=CARTESIAN_POINT ( 'NONE',  ( -4.000000000000000000, 0.3987449864459974846, -0.01220643443059782861 ) ) ;
#2710=CONICAL_SURFACE ( 'NONE', #16394, 5.560781378645573980, 1.221730476396046816 ) ;
#2716=CARTESIAN_POINT ( 'NONE',  ( -6.473970235329672780E-16, -4.862606272033106691, -3.745885042887442395 ) ) ;
#2722=CARTESIAN_POINT ( 'NONE',  ( 4.000000000000000000, 2.309401076758497151, -5.000000000000000000 ) ) ;
#2731=ORIENTED_EDGE ( 'NONE', *, *, #14036, .T. ) ;
#2742=ORIENTED_EDGE ( 'NONE', *, *, #10162, .F. ) ;
#2746=CARTESIAN_POINT ( 'NONE',  ( -4.000000000000000000, -7.806255641895631925E-15, -3.142992957459232350 ) ) ;
#2750=CARTESIAN_POINT ( 'NONE',  ( 1.393927851585479161, -4.043713361053543842, -3.526374918436840922 ) ) ;
#2767=CARTESIAN_POINT ( 'NONE',  ( -4.203934362469166963, -1.640673743454851286, -3.598432614606932756 ) ) ;
#2785=B_SPLINE_CURVE_WITH_KNOTS ( 'NONE', 3,
 ( #4840, #6164, #12169, #16261, #17977, #358 ),
 .UNSPECIFIED., .F., .F.,
 ( 4, 2, 4 ),
 ( -3.640115492410698714E-06, 0.0002066546034003381217, 0.0004169493222930869755 ),
 .UNSPECIFIED. ) ;
#2786=CARTESIAN_POINT ( 'NONE',  ( 4.000000000000000000, 0.9868501483902631932, -0.09357334158579604100 ) ) ;
#2812=LINE ( 'NONE', #2722, #12897 ) ;
#2815=ORIENTED_EDGE ( 'NONE', *, *, #13104, .T. ) ;
#2817=PRESENTATION_STYLE_ASSIGNMENT (( #63 ) ) ;
#2818=VERTEX_POINT ( 'NONE', #1503 ) ;
#2837=EDGE_LOOP ( 'NONE', ( #14120, #10715 ) ) ;
#2857=CARTESIAN_POINT ( 'NONE',  ( -4.000000000000000000, -2.512220745329312610, -3.469390707569719901 ) ) ;
#2860=CARTESIAN_POINT ( 'NONE',  ( -1.144235203016679359, -3.958177651039096911, -0.09382832055446428676 ) ) ;
#2876=LINE ( 'NONE', #11553, #2632 ) ;
#2911=DIRECTION ( 'NONE',  ( 0.8660254037844379305, 0.5000000000000013323, 0.000000000000000000 ) ) ;
#2942=MECHANICAL_DESIGN_GEOMETRIC_PRESENTATION_REPRESENTATION('',(#18751),#11458);
#2957=CARTESIAN_POINT ( 'NONE',  ( -0.3198814748697807464, -4.434118497892185040, -0.3507732604232532969 ) ) ;
#2993=VERTEX_POINT ( 'NONE', #14055 ) ;
#2997=DIRECTION ( 'NONE',  ( -0.000000000000000000, -0.000000000000000000, 1.000000000000000000 ) ) ;
#3001=CARTESIAN_POINT ( 'NONE',  ( -0.6507732100473471171, 4.243078065514775510, -0.2236248678334823436 ) ) ;
#3023=ORIENTED_EDGE ( 'NONE', *, *, #4574, .F. ) ;
#3033=EDGE_CURVE ( 'NONE', #11704, #15321, #9938, .T. ) ;
#3035=CONICAL_SURFACE ( 'NONE', #10930, 4.000000000000000000, 0.8911886515913786111 ) ;
#3051=CARTESIAN_POINT ( 'NONE',  ( 5.560781378645575757, 0.000000000000000000, -4.000000000000000000 ) ) ;
#3078=EDGE_CURVE ( 'NONE', #11483, #14252, #8058, .T. ) ;
#3107=CARTESIAN_POINT ( 'NONE',  ( 8.673617379884035472E-16, 4.618802153517012954, 0.000000000000000000 ) ) ;
#3117=CARTESIAN_POINT ( 'NONE',  ( 0.3461262719736147297, -4.658553426539303821, -3.671615880910379381 ) ) ;
#3136=CARTESIAN_POINT ( 'NONE',  ( -4.000000000000000000, 0.8576368993457507139, -3.433240632782198709 ) ) ;
#3139=CARTESIAN_POINT ( 'NONE',  ( 2.345747346278113987, -3.264484291692503870, -0.01223254789874484924 ) ) ;
#3150=ORIENTED_EDGE ( 'NONE', *, *, #7870, .T. ) ;
#3159=DIRECTION ( 'NONE',  ( 1.000000000000000000, 0.000000000000000000, 0.000000000000000000 ) ) ;
#3195=ADVANCED_FACE ( 'NONE', ( #5849 ), #12038, .F. ) ;
#3260=AXIS2_PLACEMENT_3D ( 'NONE', #16931, #3880, #1495 ) ;
#3299=CARTESIAN_POINT ( 'NONE',  ( 2.344047193898588954, 3.265465875126468021, -5.031375706690542042E-16 ) ) ;
#3308=ADVANCED_FACE ( 'NONE', ( #1570 ), #1407, .T. ) ;
#3334=CARTESIAN_POINT ( 'NONE',  ( 2.691179338796023329E-15, 4.647089433458991614, -3.572167766733753691 ) ) ;
#3336=AXIS2_PLACEMENT_3D ( 'NONE', #14368, #7116, #7217 ) ;
#3343=ORIENTED_EDGE ( 'NONE', *, *, #1461, .F. ) ;
#3372=CARTESIAN_POINT ( 'NONE',  ( 4.000000000000000000, 2.309401076758497151, -3.433295621305379353 ) ) ;
#3376=EDGE_CURVE ( 'NONE', #12396, #16921, #15699, .T. ) ;
#3391=CARTESIAN_POINT ( 'NONE',  ( 1.655952806101427033, -3.662737355149048302, -1.182683869819604841E-14 ) ) ;
#3399=CARTESIAN_POINT ( 'NONE',  ( 2.500000000000000444, 0.000000000000000000, -5.000000000000000888 ) ) ;
#3440=CARTESIAN_POINT ( 'NONE',  ( -3.264624719419710521E-13, -4.796980096169328966, -3.721999068284310486 ) ) ;
#3445=CARTESIAN_POINT ( 'NONE',  ( -4.211140560182196957, -2.431303136016552013, -3.745885042887436178 ) ) ;
#3462=DIRECTION ( 'NONE',  ( -1.000000000000000000, 0.000000000000000000, 0.000000000000000000 ) ) ;
#3481=DIRECTION ( 'NONE',  ( 0.000000000000000000, 0.000000000000000000, -1.000000000000000000 ) ) ;
#3482=CARTESIAN_POINT ( 'NONE',  ( 4.211140560182196957, -2.431303136016555122, -3.745885042887436622 ) ) ;
#3499=CARTESIAN_POINT ( 'NONE',  ( 2.712762565639649015, -3.052587955997662306, -3.430618716626630871 ) ) ;
#3506=CARTESIAN_POINT ( 'NONE',  ( 0.000000000000000000, 0.000000000000000000, 0.000000000000000000 ) ) ;
#3518=CARTESIAN_POINT ( 'NONE',  ( 0.000000000000000000, 0.000000000000000000, -4.694516984716113228 ) ) ;
#3528=ORIENTED_EDGE ( 'NONE', *, *, #18676, .F. ) ;
#3550=ORIENTED_EDGE ( 'NONE', *, *, #427, .T. ) ;
#3572=EDGE_LOOP ( 'NONE', ( #7108, #17752, #14808, #13191 ) ) ;
#3603=AXIS2_PLACEMENT_3D ( 'NONE', #17645, #14684, #399 ) ;
#3609=CARTESIAN_POINT ( 'NONE',  ( 0.5449313310647804220, 4.304185902836899835, -3.316620875263383894 ) ) ;
#3623=( BOUNDED_SURFACE ( )  B_SPLINE_SURFACE ( 3, 2, ( 
 ( #2384, #13143, #187 ),
 ( #5717, #17427, #1425 ),
 ( #1697, #3136, #281 ),
 ( #4378, #4560, #10181 ),
 ( #11805, #13332, #2767 ),
 ( #2857, #11532, #14744 ) ),
 .UNSPECIFIED., .F., .F., .F. ) 
 B_SPLINE_SURFACE_WITH_KNOTS ( ( 4, 2, 4 ),
 ( 3, 3 ),
 ( 0.02027752710269158445, 0.02273781595091097299, 0.02519810479913036153 ),
 ( 0.000000000000000000, 1.000000000000000000 ),
 .UNSPECIFIED. ) 
 GEOMETRIC_REPRESENTATION_ITEM ( )  RATIONAL_B_SPLINE_SURFACE ( (
 ( 1.000000000000000000, 0.8047781431712808242, 1.000000000000000000),
 ( 1.000000000000000000, 0.8123773247083928561, 1.000000000000000000),
 ( 1.000000000000000000, 0.8190670192154906326, 1.000000000000000000),
 ( 1.000000000000000000, 0.8192353552912178261, 1.000000000000000000),
 ( 1.000000000000000000, 0.8126132098226825917, 1.000000000000000000),
 ( 1.000000000000000000, 0.8047712465856394770, 1.000000000000000000) ) ) 
 REPRESENTATION_ITEM ( '' )  SURFACE ( )  );
#3639=CARTESIAN_POINT ( 'NONE',  ( -4.140404888673278272, -2.228338276487456415, -3.686887068327035166 ) ) ;
#3666=CARTESIAN_POINT ( 'NONE',  ( -2.000000000000007550, -3.464101615137749945, 0.000000000000000000 ) ) ;
#3685=CARTESIAN_POINT ( 'NONE',  ( 2.000000000000008882, 3.464101615137749945, 0.000000000000000000 ) ) ;
#3693=MANIFOLD_SOLID_BREP ( 'EndChamfer', #11944 ) ;
#3723=PLANE ( 'NONE',  #820 ) ;
#3783=PLANE ( 'NONE',  #16288 ) ;
#3800=CARTESIAN_POINT ( 'NONE',  ( -2.100000000000000089, 2.571758278209441957E-16, -5.000000000000000000 ) ) ;
#3813=CARTESIAN_POINT ( 'NONE',  ( 4.000000000000000000, 2.309401076758497151, -5.000000000000000000 ) ) ;
#3828=VERTEX_POINT ( 'NONE', #5604 ) ;
#3880=DIRECTION ( 'NONE',  ( -0.5000000000000019984, -0.8660254037844375974, 0.000000000000000000 ) ) ;
#3886=ADVANCED_FACE ( 'NONE', ( #1594 ), #784, .F. ) ;
#3889=CARTESIAN_POINT ( 'NONE',  ( 1.274258131564866448, 3.883108878240963513, -3.220599429844046568 ) ) ;
#3894=CARTESIAN_POINT ( 'NONE',  ( -4.000000000000000000, -2.309401076758515803, -0.4999999999999995559 ) ) ;
#3917=CARTESIAN_POINT ( 'NONE',  ( 4.000000000001088907, 1.658577278524410170, -3.531553309554541720 ) ) ;
#3923=AXIS2_PLACEMENT_3D ( 'NONE', #900, #5064, #1073 ) ;
#3973=ORIENTED_EDGE ( 'NONE', *, *, #16131, .T. ) ;
#4027=B_SPLINE_CURVE_WITH_KNOTS ( 'NONE', 3,
 ( #17495, #6062, #4633, #14638, #2750, #15799, #3117, #10353 ),
 .UNSPECIFIED., .F., .F.,
 ( 4, 2, 2, 4 ),
 ( 0.000000000000000000, 0.002450665683189819262, 0.003675998524784728893, 0.004901331366379639391 ),
 .UNSPECIFIED. ) ;
#4085=ORIENTED_EDGE ( 'NONE', *, *, #16122, .T. ) ;
#4091=CARTESIAN_POINT ( 'NONE',  ( -3.999999999999999112, -2.309401076758512694, -3.504269196027871125 ) ) ;
#4097=DIRECTION ( 'NONE',  ( -0.000000000000000000, -0.000000000000000000, 1.000000000000000000 ) ) ;
#4129=CARTESIAN_POINT ( 'NONE',  ( -4.000000000000000000, 0.000000000000000000, 0.000000000000000000 ) ) ;
#4134=ORIENTED_EDGE ( 'NONE', *, *, #16131, .F. ) ;
#4170=VERTEX_POINT ( 'NONE', #18055 ) ;
#4204=DIRECTION ( 'NONE',  ( 0.000000000000000000, 0.000000000000000000, 1.000000000000000000 ) ) ;
#4261=( LENGTH_UNIT ( ) NAMED_UNIT ( * ) SI_UNIT ( .MILLI., .METRE. ) );
#4268=CARTESIAN_POINT ( 'NONE',  ( 0.000000000000000000, 0.000000000000000000, 0.000000000000000000 ) ) ;
#4288=ORIENTED_EDGE ( 'NONE', *, *, #13070, .F. ) ;
#4315=CARTESIAN_POINT ( 'NONE',  ( 0.000000000000000000, 0.000000000000000000, 0.000000000000000000 ) ) ;
#4336=DIRECTION ( 'NONE',  ( 0.000000000000000000, 0.000000000000000000, 1.000000000000000000 ) ) ;
#4362=EDGE_LOOP ( 'NONE', ( #3150, #9156 ) ) ;
#4366=ORIENTED_EDGE ( 'NONE', *, *, #9818, .F. ) ;
#4367=CARTESIAN_POINT ( 'NONE',  ( 4.000000000000000000, 2.309401076758497151, -5.000000000000000000 ) ) ;
#4378=CARTESIAN_POINT ( 'NONE',  ( -4.000000000000000000, -0.8382240730041925492, -3.220610619767135141 ) ) ;
#4388=EDGE_CURVE ( 'NONE', #16102, #4891, #10093, .T. ) ;
#4403=CYLINDRICAL_SURFACE ( 'NONE', #10590, 2.100000000000000089 ) ;
#4411=LINE ( 'NONE', #8519, #15149 ) ;
#4417=EDGE_LOOP ( 'NONE', ( #16850, #18187, #10692, #6710, #7547 ) ) ;
#4433=DIRECTION ( 'NONE',  ( -1.000000000000000000, 0.000000000000000000, 0.000000000000000000 ) ) ;
#4443=CARTESIAN_POINT ( 'NONE',  ( -4.000000000000000000, 2.309401076758498483, -5.000000000000000000 ) ) ;
#4452=DIRECTION ( 'NONE',  ( 0.5000000000000022204, 0.8660254037844374864, -0.000000000000000000 ) ) ;
#4471=CARTESIAN_POINT ( 'NONE',  ( -4.000000000000000000, -2.309401076758512694, -3.433295621305382461 ) ) ;
#4522=DIRECTION ( 'NONE',  ( 1.000000000000000000, 0.000000000000000000, 0.000000000000000000 ) ) ;
#4533=ADVANCED_FACE ( 'NONE', ( #11174 ), #13754, .T. ) ;
#4560=CARTESIAN_POINT ( 'NONE',  ( -4.000000000000000000, -0.8232339106130515116, -3.430630286862743183 ) ) ;
#4574=EDGE_CURVE ( 'NONE', #13860, #11877, #18493, .T. ) ;
#4607=CARTESIAN_POINT ( 'NONE',  ( 0.000000000000000000, 0.000000000000000000, -4.000000000000000000 ) ) ;
#4615=CARTESIAN_POINT ( 'NONE',  ( -3.680118525130244400, 2.494084732383327285, -0.3507732604232449702 ) ) ;
#4633=CARTESIAN_POINT ( 'NONE',  ( 2.805705207896068476, -3.226868319750173075, -3.503898532754370354 ) ) ;
#4650=EDGE_LOOP ( 'NONE', ( #17700, #17577, #9418, #7806 ) ) ;
#4660=ADVANCED_FACE ( 'NONE', ( #18607 ), #9846, .T. ) ;
#4677=CARTESIAN_POINT ( 'NONE',  ( 0.000000000000000000, 0.000000000000000000, -25.03750572909317285 ) ) ;
#4698=CARTESIAN_POINT ( 'NONE',  ( 4.211140560182196957, 2.431303136016536470, -3.745885042887433514 ) ) ;
#4716=EDGE_LOOP ( 'NONE', ( #13734, #4288, #16408 ) ) ;
#4741=CARTESIAN_POINT ( 'NONE',  ( -3.974357786152442180E-13, 4.796734841935204052, -3.721909803043259579 ) ) ;
#4771=ORIENTED_EDGE ( 'NONE', *, *, #9423, .T. ) ;
#4779=AXIS2_PLACEMENT_3D ( 'NONE', #18068, #9407, #18167 ) ;
#4820=CARTESIAN_POINT ( 'NONE',  ( 3.349226789952652439, 2.685125164760731487, -0.2236248678334773199 ) ) ;
#4838=AXIS2_PLACEMENT_3D ( 'NONE', #18488, #14472, #8490 ) ;
#4840=CARTESIAN_POINT ( 'NONE',  ( -4.211140560182196957, 2.431303136016537803, -3.745885042887433514 ) ) ;
#4850=CARTESIAN_POINT ( 'NONE',  ( 4.211140560182196957, 2.431303136016536470, -3.745885042887433514 ) ) ;
#4891=VERTEX_POINT ( 'NONE', #7126 ) ;
#4892=CARTESIAN_POINT ( 'NONE',  ( 4.000000000000000000, -2.309401076758514915, -3.433295621305383349 ) ) ;
#4895=CARTESIAN_POINT ( 'NONE',  ( 0.6920835326022565237, 4.454600218803884459, -3.597382984111579862 ) ) ;
#4909=CONICAL_SURFACE ( 'NONE', #13133, 4.000000000000000000, 0.8911886515913786111 ) ;
#4917=FACE_OUTER_BOUND ( 'NONE', #8910, .T. ) ;
#4926=ORIENTED_EDGE ( 'NONE', *, *, #12852, .T. ) ;
#4932=CARTESIAN_POINT ( 'NONE',  ( -4.211140560182196957, -2.431303136016552013, -3.745885042887436178 ) ) ;
#4955=ORIENTED_EDGE ( 'NONE', *, *, #10360, .F. ) ;
#4999=ORIENTED_EDGE ( 'NONE', *, *, #9818, .T. ) ;
#5004=PRODUCT_DEFINITION_FORMATION_WITH_SPECIFIED_SOURCE ( 'ANY', '', #9804, .NOT_KNOWN. ) ;
#5011=CARTESIAN_POINT ( 'NONE',  ( 2.836893136758676270, 3.208949435745843903, -3.505054077164911241 ) ) ;
#5023=CARTESIAN_POINT ( 'NONE',  ( -4.101948962586059899, -2.368261337751176754, -3.681124513963741851 ) ) ;
#5037=CARTESIAN_POINT ( 'NONE',  ( 4.000000000000000000, -2.471525695159793035, -3.686886880705770864 ) ) ;
#5041=( BOUNDED_SURFACE ( )  B_SPLINE_SURFACE ( 3, 2, ( 
 ( #8288, #5037, #582 ),
 ( #13722, #5323, #2278 ),
 ( #15330, #6573, #7907 ),
 ( #18091, #18373, #2473 ),
 ( #6387, #3917, #16961 ),
 ( #12282, #673, #17999 ) ),
 .UNSPECIFIED., .F., .F., .F. ) 
 B_SPLINE_SURFACE_WITH_KNOTS ( ( 4, 2, 4 ),
 ( 3, 3 ),
 ( 0.02027065861071770947, 0.02273072267836921331, 0.02519078674602071716 ),
 ( 0.000000000000000000, 1.000000000000000000 ),
 .UNSPECIFIED. ) 
 GEOMETRIC_REPRESENTATION_ITEM ( )  RATIONAL_B_SPLINE_SURFACE ( (
 ( 1.000000000000000000, 0.8047781708337304885, 1.000000000000000000),
 ( 1.000000000000000000, 0.8123765190705307671, 1.000000000000000000),
 ( 1.000000000000000000, 0.8190656277163975707, 1.000000000000000000),
 ( 1.000000000000000000, 0.8192366903512159348, 1.000000000000000000),
 ( 1.000000000000000000, 0.8126138454302893610, 1.000000000000000000),
 ( 1.000000000000000000, 0.8047712246031417660, 1.000000000000000000) ) ) 
 REPRESENTATION_ITEM ( '' )  SURFACE ( )  );
#5047=CARTESIAN_POINT ( 'NONE',  ( -5.560781378645573980, 0.000000000000000000, -4.000000000000000000 ) ) ;
#5064=DIRECTION ( 'NONE',  ( 0.000000000000000000, 0.000000000000000000, -1.000000000000000000 ) ) ;
#5078=VERTEX_POINT ( 'NONE', #13421 ) ;
#5085=AXIS2_PLACEMENT_3D ( 'NONE', #11017, #13885, #18557 ) ;
#5138=EDGE_LOOP ( 'NONE', ( #16498, #12689, #18685, #2355, #11119 ) ) ;
#5175=DIRECTION ( 'NONE',  ( -0.000000000000000000, 0.000000000000000000, -1.000000000000000000 ) ) ;
#5182=CARTESIAN_POINT ( 'NONE',  ( 1.411581201560190495E-15, 4.862606272033091592, -3.745885042887436622 ) ) ;
#5187=DIRECTION ( 'NONE',  ( 0.000000000000000000, 0.000000000000000000, 1.000000000000000000 ) ) ;
#5210=CARTESIAN_POINT ( 'NONE',  ( 3.540020015735602765, 2.810662092924382627, -3.602146406945867962 ) ) ;
#5214=CARTESIAN_POINT ( 'NONE',  ( 1.567478505476134606E-15, 4.618802153517012066, -3.433295621305382905 ) ) ;
#5225=VECTOR ( 'NONE', #5429, 1000.000000000000000 ) ;
#5232=DIRECTION ( 'NONE',  ( 0.000000000000000000, 0.000000000000000000, -1.000000000000000000 ) ) ;
#5238=CARTESIAN_POINT ( 'NONE',  ( 0.000000000000000000, 0.000000000000000000, -4.974599999999998801 ) ) ;
#5255=CARTESIAN_POINT ( 'NONE',  ( 0.000000000000000000, 0.000000000000000000, 0.000000000000000000 ) ) ;
#5263=FACE_OUTER_BOUND ( 'NONE', #5313, .T. ) ;
#5271=B_SPLINE_CURVE_WITH_KNOTS ( 'NONE', 3,
 ( #11890, #2957, #14468, #2860, #7234, #16470, #9415, #10829 ),
 .UNSPECIFIED., .F., .F.,
 ( 4, 2, 2, 4 ),
 ( 2.465131517390770070E-07, 0.001183067374689869946, 0.001774477805458935659, 0.002365888236228001588 ),
 .UNSPECIFIED. ) ;
#5274=EDGE_CURVE ( 'NONE', #13860, #5078, #11157, .T. ) ;
#5280=DIRECTION ( 'NONE',  ( -1.000000000000000000, 0.000000000000000000, 0.000000000000000000 ) ) ;
#5282=VERTEX_POINT ( 'NONE', #12591 ) ;
#5288=CARTESIAN_POINT ( 'NONE',  ( 5.384454397937118664, 0.000000000000000000, -5.000000000000000000 ) ) ;
#5300=CARTESIAN_POINT ( 'NONE',  ( -2.000000000000002665, -3.464101615137770374, -3.142992957459237680 ) ) ;
#5305=EDGE_LOOP ( 'NONE', ( #825, #441, #17003, #4366 ) ) ;
#5313=EDGE_LOOP ( 'NONE', ( #14084, #999, #17764, #4134 ) ) ;
#5319=EDGE_CURVE ( 'NONE', #12639, #18552, #1643, .T. ) ;
#5323=CARTESIAN_POINT ( 'NONE',  ( 4.000000000000000000, -1.677850389431204459, -3.535268758346977513 ) ) ;
#5346=EDGE_LOOP ( 'NONE', ( #18067, #15296, #1766, #1034, #9961 ) ) ;
#5369=CARTESIAN_POINT ( 'NONE',  ( -4.000000000000000000, -2.309401076758515803, -0.4999999999999995559 ) ) ;
#5387=CARTESIAN_POINT ( 'NONE',  ( 0.000000000000000000, 0.000000000000000000, -0.2800830152838844622 ) ) ;
#5421=ADVANCED_FACE ( 'NONE', ( #17982 ), #8738, .T. ) ;
#5429=DIRECTION ( 'NONE',  ( 0.000000000000000000, 0.000000000000000000, 1.000000000000000000 ) ) ;
#5430=CIRCLE ( 'NONE', #7845, 5.384454397937118664 ) ;
#5442=AXIS2_PLACEMENT_3D ( 'NONE', #3518, #10745, #16477 ) ;
#5455=AXIS2_PLACEMENT_3D ( 'NONE', #4677, #124, #3159 ) ;
#5484=CARTESIAN_POINT ( 'NONE',  ( 4.211140560182196957, -2.431303136016555122, -3.745885042887436622 ) ) ;
#5502=FACE_OUTER_BOUND ( 'NONE', #11906, .T. ) ;
#5524=ADVANCED_FACE ( 'NONE', ( #16842 ), #1160, .T. ) ;
#5537=LINE ( 'NONE', #8483, #16804 ) ;
#5546=ORIENTED_EDGE ( 'NONE', *, *, #18702, .T. ) ;
#5604=CARTESIAN_POINT ( 'NONE',  ( -2.499999999999999556, 3.061616997868382648E-16, 3.469446951953614189E-15 ) ) ;
#5611=ORIENTED_EDGE ( 'NONE', *, *, #18422, .T. ) ;
#5618=DIRECTION ( 'NONE',  ( 1.000000000000000000, 0.000000000000000000, 0.000000000000000000 ) ) ;
#5635=LINE ( 'NONE', #15639, #6094 ) ;
#5660=CARTESIAN_POINT ( 'NONE',  ( 4.207491450040567571, -2.029819825146485179, -3.671670828759567407 ) ) ;
#5693=CARTESIAN_POINT ( 'NONE',  ( -3.999999999999999112, 1.539600717838996324, -3.300726591567078039 ) ) ;
#5717=CARTESIAN_POINT ( 'NONE',  ( -4.000000000000000000, 1.700094919196744270, -3.320312364301766017 ) ) ;
#5753=CIRCLE ( 'NONE', #14262, 5.560781378645573980 ) ;
#5772=DIRECTION ( 'NONE',  ( 1.000000000000000000, 0.000000000000000000, 0.000000000000000000 ) ) ;
#5829=DIRECTION ( 'NONE',  ( -1.000000000000000000, 0.000000000000000000, 0.000000000000000000 ) ) ;
#5844=DIRECTION ( 'NONE',  ( 0.000000000000000000, 0.000000000000000000, 1.000000000000000000 ) ) ;
#5849=FACE_OUTER_BOUND ( 'NONE', #1086, .T. ) ;
#5963=ORIENTED_EDGE ( 'NONE', *, *, #7952, .T. ) ;
#5964=ORIENTED_EDGE ( 'NONE', *, *, #7124, .F. ) ;
#6004=CARTESIAN_POINT ( 'NONE',  ( -6.259644161404859044E-16, -4.618802153517026277, -3.504271511727133248 ) ) ;
#6016=CARTESIAN_POINT ( 'NONE',  ( -4.204015924366189871, 1.626724848190922446, -3.610627190413390419 ) ) ;
#6018=B_SPLINE_CURVE_WITH_KNOTS ( 'NONE', 3,
 ( #17788, #4741, #16376, #3334, #6266, #13614 ),
 .UNSPECIFIED., .F., .F.,
 ( 4, 2, 4 ),
 ( -3.640115492407174633E-06, 0.0002066546034003413743, 0.0004169493222930899571 ),
 .UNSPECIFIED. ) ;
#6025=EDGE_CURVE ( 'NONE', #7169, #5282, #5430, .T. ) ;
#6027=CARTESIAN_POINT ( 'NONE',  ( 3.999999999999999112, 2.309401076758497595, -3.504271511727124366 ) ) ;
#6046=FILL_AREA_STYLE ('',( #10059 ) ) ;
#6056=CARTESIAN_POINT ( 'NONE',  ( 0.6507732100473444525, -4.243078065514795050, -0.2236248678334952777 ) ) ;
#6062=CARTESIAN_POINT ( 'NONE',  ( 3.511755186886750923, -2.826662030176382956, -3.597382984111582083 ) ) ;
#6094=VECTOR ( 'NONE', #12497, 999.9999999999998863 ) ;
#6127=CARTESIAN_POINT ( 'NONE',  ( 3.333333333333332593, 2.694301256218250007, -3.300726591567078483 ) ) ;
#6135=CARTESIAN_POINT ( 'NONE',  ( -3.355112389629170799, 2.681727112203152963, -0.2256878752776689534 ) ) ;
#6145=ORIENTED_EDGE ( 'NONE', *, *, #18432, .T. ) ;
#6149=UNCERTAINTY_MEASURE_WITH_UNIT (LENGTH_MEASURE( 1.000000000000000082E-05 ), #9900, 'distance_accuracy_value', 'NONE');
#6153=CARTESIAN_POINT ( 'NONE',  ( -3.455068668934486276, 2.624017327439035707, -3.316620875263955437 ) ) ;
#6164=CARTESIAN_POINT ( 'NONE',  ( -4.154094228333542915, 2.398367420968061658, -3.721909803043254694 ) ) ;
#6184=B_SPLINE_CURVE_WITH_KNOTS ( 'NONE', 3,
 ( #4850, #10655, #6464, #18076 ),
 .UNSPECIFIED., .F., .F.,
 ( 4, 4 ),
 ( 0.000000000000000000, 0.002452478801916361129 ),
 .UNSPECIFIED. ) ;
#6214=EDGE_CURVE ( 'NONE', #7704, #2818, #10478, .T. ) ;
#6221=CARTESIAN_POINT ( 'NONE',  ( 0.000000000000000000, 0.000000000000000000, -4.484454397937119197 ) ) ;
#6222=CARTESIAN_POINT ( 'NONE',  ( 2.804994570502171047, 3.229033611042449792, -3.526374918436834704 ) ) ;
#6229=( GEOMETRIC_REPRESENTATION_CONTEXT ( 3 ) GLOBAL_UNCERTAINTY_ASSIGNED_CONTEXT ( ( #76 ) ) GLOBAL_UNIT_ASSIGNED_CONTEXT ( ( #4261, #8533, #16150 ) ) REPRESENTATION_CONTEXT ( 'NONE', 'WORKASPACE' ) );
#6231=EDGE_LOOP ( 'NONE', ( #11120, #15451, #9633, #18703, #12842 ) ) ;
#6246=CARTESIAN_POINT ( 'NONE',  ( -3.522875095019672109, 2.820352903225427532, -3.598441714920591394 ) ) ;
#6249=EDGE_CURVE ( 'NONE', #17591, #4170, #5753, .T. ) ;
#6266=CARTESIAN_POINT ( 'NONE',  ( 1.567478505476134803E-15, 4.618802153517012954, -3.504269196027872457 ) ) ;
#6305=AXIS2_PLACEMENT_3D ( 'NONE', #3506, #9127, #16267 ) ;
#6323=CARTESIAN_POINT ( 'NONE',  ( 3.861362476283255685, 2.629030857715988656, -3.671615880910370500 ) ) ;
#6387=CARTESIAN_POINT ( 'NONE',  ( 4.000000000000000000, 1.680228229147133767, -3.316631783032546021 ) ) ;
#6439=CIRCLE ( 'NONE', #16479, 2.499999999999999556 ) ;
#6442=CARTESIAN_POINT ( 'NONE',  ( -2.712762565639006418, 3.052587955997511759, -3.430618716626627318 ) ) ;
#6464=CARTESIAN_POINT ( 'NONE',  ( 4.197393957002303999, 0.8151795401431359833, -3.503767560748935139 ) ) ;
#6486=DIRECTION ( 'NONE',  ( -0.9396926207859138680, 0.000000000000000000, -0.3420201433256536139 ) ) ;
#6492=ORIENTED_EDGE ( 'NONE', *, *, #7937, .T. ) ;
#6511=CARTESIAN_POINT ( 'NONE',  ( -2.344047193898593395, -3.265465875126480455, -1.054683074273691752E-14 ) ) ;
#6513=CARTESIAN_POINT ( 'NONE',  ( 0.000000000000000000, 0.000000000000000000, -5.000000000000000888 ) ) ;
#6519=ORIENTED_EDGE ( 'NONE', *, *, #17359, .F. ) ;
#6532=ORIENTED_EDGE ( 'NONE', *, *, #1461, .T. ) ;
#6533=DIRECTION ( 'NONE',  ( -0.8660254037844373753, 0.5000000000000021094, 0.000000000000000000 ) ) ;
#6549=EDGE_CURVE ( 'NONE', #5078, #16102, #472, .T. ) ;
#6564=ADVANCED_FACE ( 'NONE', ( #14971 ), #8783, .F. ) ;
#6573=CARTESIAN_POINT ( 'NONE',  ( 4.000000000000000888, -0.8578082829538523635, -3.433262215449808696 ) ) ;
#6582=CARTESIAN_POINT ( 'NONE',  ( -4.000000000000000000, 0.000000000000000000, 0.000000000000000000 ) ) ;
#6588=AXIS2_PLACEMENT_3D ( 'NONE', #18699, #1193, #2190 ) ;
#6625=CARTESIAN_POINT ( 'NONE',  ( 4.000000000000000000, -2.309401076758514915, -3.433295621305383349 ) ) ;
#6647=FACE_OUTER_BOUND ( 'NONE', #5346, .T. ) ;
#6650=LINE ( 'NONE', #11846, #17859 ) ;
#6710=ORIENTED_EDGE ( 'NONE', *, *, #8143, .T. ) ;
#6733=CARTESIAN_POINT ( 'NONE',  ( 4.000000000000000000, 2.309401076758515803, -0.4999999999999995559 ) ) ;
#6739=CARTESIAN_POINT ( 'NONE',  ( 1.287237434362044075, 3.875615274277557809, -3.430618716626812059 ) ) ;
#6760=CARTESIAN_POINT ( 'NONE',  ( 4.000000000000000000, -1.560351142792952617, -0.2242961665059816367 ) ) ;
#6812=CARTESIAN_POINT ( 'NONE',  ( 1.144235203016666258, 3.958177651039090250, -0.09382832055445661235 ) ) ;
#6826=CARTESIAN_POINT ( 'NONE',  ( 4.140404888673277384, 2.228338276487440428, -3.686887068327033390 ) ) ;
#6832=ADVANCED_FACE ( 'NONE', ( #2196 ), #1649, .F. ) ;
#6865=AXIS2_PLACEMENT_3D ( 'NONE', #6221, #13188, #4522 ) ;
#6891=DIRECTION ( 'NONE',  ( -0.8660254037844377084, -0.5000000000000015543, 0.000000000000000000 ) ) ;
#6899=CARTESIAN_POINT ( 'NONE',  ( 4.198928548860774157, -0.8158838809860124996, -3.526471437616918170 ) ) ;
#6900=CIRCLE ( 'NONE', #12685, 2.499999999999999556 ) ;
#6921=CIRCLE ( 'NONE', #4779, 0.5155456020628804703 ) ;
#6923=PRODUCT_DEFINITION_SHAPE ( 'NONE', 'NONE',  #12243 ) ;
#6928=LINE ( 'NONE', #11501, #12809 ) ;
#6950=CONICAL_SURFACE ( 'NONE', #3923, 2.500000000000000888, 0.9599310885968785900 ) ;
#6953=ORIENTED_EDGE ( 'NONE', *, *, #11097, .T. ) ;
#6957=CARTESIAN_POINT ( 'NONE',  ( -4.211140560182196957, -2.431303136016552013, -3.745885042887436178 ) ) ;
#6960=CONICAL_SURFACE ( 'NONE', #4838, 4.000000000000000000, 0.8911886515913786111 ) ;
#6968=B_SPLINE_CURVE_WITH_KNOTS ( 'NONE', 3,
 ( #1902, #12640, #5300, #11108, #9688 ),
 .UNSPECIFIED., .F., .F.,
 ( 4, 1, 4 ),
 ( 0.000000000000000000, 0.002309401076758505356, 0.004618802153517010713 ),
 .UNSPECIFIED. ) ;
#6971=ORIENTED_EDGE ( 'NONE', *, *, #1334, .F. ) ;
#6991=DIRECTION ( 'NONE',  ( 0.000000000000000000, 0.000000000000000000, 1.000000000000000000 ) ) ;
#7044=CARTESIAN_POINT ( 'NONE',  ( -2.449848172108560540, -3.432307619358754724, -3.503702292528910078 ) ) ;
#7084=CARTESIAN_POINT ( 'NONE',  ( 4.197393957002303999, -0.4069871074557456780, -3.503767560748925813 ) ) ;
#7092=CARTESIAN_POINT ( 'NONE',  ( 1.567478505476134606E-15, 4.618802153517012066, -5.000000000000000000 ) ) ;
#7108=ORIENTED_EDGE ( 'NONE', *, *, #9592, .T. ) ;
#7116=DIRECTION ( 'NONE',  ( -0.000000000000000000, -0.000000000000000000, 1.000000000000000000 ) ) ;
#7124=EDGE_CURVE ( 'NONE', #5282, #7169, #16723, .T. ) ;
#7126=CARTESIAN_POINT ( 'NONE',  ( -2.000000000000006661, 3.464101615137750834, 0.000000000000000000 ) ) ;
#7127=CARTESIAN_POINT ( 'NONE',  ( 2.500000000000000444, 0.000000000000000000, -25.03750572909317285 ) ) ;
#7128=CARTESIAN_POINT ( 'NONE',  ( 0.000000000000000000, 0.000000000000000000, -4.484454397937119197 ) ) ;
#7133=CARTESIAN_POINT ( 'NONE',  ( 4.154306624730763176, -2.398490048084970461, -3.721999068284303824 ) ) ;
#7161=VERTEX_POINT ( 'NONE', #9861 ) ;
#7169=VERTEX_POINT ( 'NONE', #5288 ) ;
#7204=CARTESIAN_POINT ( 'NONE',  ( 1.567478505476134606E-15, 4.618802153517012066, -3.433295621305382905 ) ) ;
#7217=DIRECTION ( 'NONE',  ( 1.000000000000000000, 0.000000000000000000, 0.000000000000000000 ) ) ;
#7234=CARTESIAN_POINT ( 'NONE',  ( -1.312671235360383548, -3.860931062424228788, -0.05923475698271369466 ) ) ;
#7238=CIRCLE ( 'NONE', #3603, 2.500000000000000444 ) ;
#7286=DIRECTION ( 'NONE',  ( 0.000000000000000000, 0.000000000000000000, 1.000000000000000000 ) ) ;
#7302=B_SPLINE_CURVE_WITH_KNOTS ( 'NONE', 3,
 ( #13514, #2088, #7893, #14945, #7786, #3139, #10371, #13426 ),
 .UNSPECIFIED., .F., .F.,
 ( 4, 2, 2, 4 ),
 ( 2.465131517071610173E-07, 0.001183067374689837636, 0.001774477805458902699, 0.002365888236227967761 ),
 .UNSPECIFIED. ) ;
#7352=PRODUCT_CONTEXT ( 'NONE', #1115, 'mechanical' ) ;
#7359=CARTESIAN_POINT ( 'NONE',  ( 4.024499207728848837, 2.323545700935681246, -3.572172305156870564 ) ) ;
#7425=DIRECTION ( 'NONE',  ( -0.000000000000000000, -0.000000000000000000, 1.000000000000000000 ) ) ;
#7442=SHAPE_DEFINITION_REPRESENTATION ( #6923, #2517 ) ;
#7452=CARTESIAN_POINT ( 'NONE',  ( 1.734723475976807094E-15, 4.618802153517012954, -0.4999999999999995559 ) ) ;
#7547=ORIENTED_EDGE ( 'NONE', *, *, #6549, .T. ) ;
#7561=ORIENTED_EDGE ( 'NONE', *, *, #6249, .T. ) ;
#7564=CARTESIAN_POINT ( 'NONE',  ( 2.449848172108560096, 3.432307619358740514, -3.503702292528905637 ) ) ;
#7570=CARTESIAN_POINT ( 'NONE',  ( -2.000000000000006661, 3.464101615137750834, 0.000000000000000000 ) ) ;
#7585=CARTESIAN_POINT ( 'NONE',  ( -0.5469614295416921346, 4.303013824936271270, -3.535263753543735454 ) ) ;
#7606=B_SPLINE_CURVE_WITH_KNOTS ( 'NONE', 3,
 ( #14988, #5693, #2746, #415, #328 ),
 .UNSPECIFIED., .F., .F.,
 ( 4, 1, 4 ),
 ( 0.000000000000000000, 0.002309401076758505790, 0.004618802153517011580 ),
 .UNSPECIFIED. ) ;
#7646=CARTESIAN_POINT ( 'NONE',  ( 0.6666666666666689611, 4.233901974057261874, -3.300726591567082480 ) ) ;
#7661=CARTESIAN_POINT ( 'NONE',  ( -0.02448733951239248641, -4.877042772274742255, -3.751161874094027571 ) ) ;
#7665=ORIENTED_EDGE ( 'NONE', *, *, #10162, .T. ) ;
#7694=DIRECTION ( 'NONE',  ( -0.000000000000000000, -0.000000000000000000, 1.000000000000000000 ) ) ;
#7704=VERTEX_POINT ( 'NONE', #18696 ) ;
#7729=DIRECTION ( 'NONE',  ( -0.8191520442889875797, 1.003171929053519570E-16, 0.5735764363510522656 ) ) ;
#7742=CARTESIAN_POINT ( 'NONE',  ( -2.855764796983342624, 2.970025579236414082, -0.09382832055445475272 ) ) ;
#7774=CARTESIAN_POINT ( 'NONE',  ( 2.807080416178989513, -3.225969019225150003, -3.502507215260505014 ) ) ;
#7780=CARTESIAN_POINT ( 'NONE',  ( -4.197393957002303999, -0.8151795401431414234, -3.503767560748935139 ) ) ;
#7786=CARTESIAN_POINT ( 'NONE',  ( 2.687328764639642653, -3.067272167851299969, -0.05923475698271395140 ) ) ;
#7806=ORIENTED_EDGE ( 'NONE', *, *, #6214, .F. ) ;
#7828=ADVANCED_FACE ( 'NONE', ( #1188 ), #4403, .F. ) ;
#7845=AXIS2_PLACEMENT_3D ( 'NONE', #1378, #12816, #12719 ) ;
#7870=EDGE_CURVE ( 'NONE', #18131, #10711, #7238, .T. ) ;
#7882=CARTESIAN_POINT ( 'NONE',  ( 0.000000000000000000, 0.000000000000000000, 3.469446951953614189E-15 ) ) ;
#7890=CARTESIAN_POINT ( 'NONE',  ( 2.100000000000000089, 0.000000000000000000, -0.2800830152838844622 ) ) ;
#7893=CARTESIAN_POINT ( 'NONE',  ( 3.355112389629172576, -2.681727112203168950, -0.2256878752776777242 ) ) ;
#7907=CARTESIAN_POINT ( 'NONE',  ( 4.197478902586992966, -0.8524102783748346290, -3.505063281295504041 ) ) ;
#7909=DIRECTION ( 'NONE',  ( -0.000000000000000000, -0.000000000000000000, 1.000000000000000000 ) ) ;
#7916=CARTESIAN_POINT ( 'NONE',  ( -4.000000000000000000, -2.309401076758515803, -0.4999999999999995559 ) ) ;
#7937=EDGE_CURVE ( 'NONE', #11956, #7161, #10658, .T. ) ;
#7941=CARTESIAN_POINT ( 'NONE',  ( -3.511755186886750479, 2.826662030176366081, -3.597382984111578086 ) ) ;
#7952=EDGE_CURVE ( 'NONE', #18552, #16201, #9753, .T. ) ;
#7957=DIRECTION ( 'NONE',  ( 1.000000000000000000, 0.000000000000000000, 0.000000000000000000 ) ) ;
#7996=CARTESIAN_POINT ( 'NONE',  ( 3.999999999999999112, -0.3979232138631231819, -5.929230630780099908E-17 ) ) ;
#8002=CARTESIAN_POINT ( 'NONE',  ( -4.235886605889389145, -2.417314728048544303, -3.751161874094020909 ) ) ;
#8017=AXIS2_PLACEMENT_3D ( 'NONE', #12801, #14324, #9934 ) ;
#8019=CARTESIAN_POINT ( 'NONE',  ( 2.000000000000005329, -3.464101615137751722, 0.000000000000000000 ) ) ;
#8058=B_SPLINE_CURVE_WITH_KNOTS ( 'NONE', 3,
 ( #9567, #15383, #926, #6812, #10805, #16823, #16627, #3685 ),
 .UNSPECIFIED., .F., .F.,
 ( 4, 2, 2, 4 ),
 ( 2.465131517075058656E-07, 0.001183067374689851080, 0.001774477805458923299, 0.002365888236227995517 ),
 .UNSPECIFIED. ) ;
#8091=EDGE_CURVE ( 'NONE', #18552, #4170, #13640, .T. ) ;
#8102=CARTESIAN_POINT ( 'NONE',  ( -2.100000000000000089, 2.571758278209441957E-16, -4.694516984716113228 ) ) ;
#8137=CARTESIAN_POINT ( 'NONE',  ( -0.6937372685066653943, 4.453844082567723461, -3.610536846335889116 ) ) ;
#8143=EDGE_CURVE ( 'NONE', #11877, #5078, #14503, .T. ) ;
#8167=DIRECTION ( 'NONE',  ( 0.5000000000000013323, -0.8660254037844379305, 0.000000000000000000 ) ) ;
#8197=ADVANCED_FACE ( 'NONE', ( #9821 ), #6960, .T. ) ;
#8249=EDGE_LOOP ( 'NONE', ( #17849, #10842, #5611, #2417, #17451 ) ) ;
#8270=CARTESIAN_POINT ( 'NONE',  ( 0.6810597143197052450, 4.461075778259290914, -3.598441714920602053 ) ) ;
#8288=CARTESIAN_POINT ( 'NONE',  ( 4.000000000000000000, -2.511475576507276042, -3.469253905236643565 ) ) ;
#8296=CARTESIAN_POINT ( 'NONE',  ( 4.000000000000003553, -2.309401076758513138, -3.504271511727127031 ) ) ;
#8358=DIRECTION ( 'NONE',  ( -1.000000000000000000, 0.000000000000000000, 0.000000000000000000 ) ) ;
#8365=EDGE_LOOP ( 'NONE', ( #11090, #15634, #6145, #16264, #1631 ) ) ;
#8445=AXIS2_PLACEMENT_3D ( 'NONE', #6513, #13950, #18321 ) ;
#8457=DIRECTION ( 'NONE',  ( 0.9396926207859138680, 1.150791560227856926E-16, -0.3420201433256536139 ) ) ;
#8478=CARTESIAN_POINT ( 'NONE',  ( -0.6920835326022555245, -4.454600218803899558, -3.597382984111586079 ) ) ;
#8483=CARTESIAN_POINT ( 'NONE',  ( 4.000000000000000000, -2.309401076758514915, -5.000000000000000000 ) ) ;
#8485=CARTESIAN_POINT ( 'NONE',  ( 4.101954839143203912, -2.368264730583031330, -3.681130640444377988 ) ) ;
#8490=DIRECTION ( 'NONE',  ( -1.000000000000000000, 0.000000000000000000, 0.000000000000000000 ) ) ;
#8493=ORIENTED_EDGE ( 'NONE', *, *, #4388, .F. ) ;
#8496=EDGE_CURVE ( 'NONE', #12688, #11921, #13053, .T. ) ;
#8503=AXIS2_PLACEMENT_3D ( 'NONE', #1016, #7694, #12531 ) ;
#8507=CARTESIAN_POINT ( 'NONE',  ( -4.000000000000000000, 0.7924765000094600165, -0.05906175389889745803 ) ) ;
#8519=CARTESIAN_POINT ( 'NONE',  ( -4.000000000000000000, -2.309401076758512694, -5.000000000000000000 ) ) ;
#8528=ORIENTED_EDGE ( 'NONE', *, *, #8714, .T. ) ;
#8529=EDGE_LOOP ( 'NONE', ( #6971, #4771, #12391, #4085, #12417, #9931, #8528 ) ) ;
#8533=( NAMED_UNIT ( * ) PLANE_ANGLE_UNIT ( ) SI_UNIT ( $, .RADIAN. ) );
#8552=DIRECTION ( 'NONE',  ( 0.000000000000000000, 0.000000000000000000, 1.000000000000000000 ) ) ;
#8567=DIRECTION ( 'NONE',  ( 0.000000000000000000, 0.000000000000000000, -1.000000000000000000 ) ) ;
#8587=CARTESIAN_POINT ( 'NONE',  ( 4.000000000000000000, 2.309401076758515803, -0.4999999999999995559 ) ) ;
#8597=CARTESIAN_POINT ( 'NONE',  ( 0.000000000000000000, 0.000000000000000000, -5.000000000000000000 ) ) ;
#8625=EDGE_CURVE ( 'NONE', #12639, #2269, #16764, .T. ) ;
#8630=ORIENTED_EDGE ( 'NONE', *, *, #3078, .F. ) ;
#8677=ORIENTED_EDGE ( 'NONE', *, *, #964, .T. ) ;
#8686=ORIENTED_EDGE ( 'NONE', *, *, #11792, .F. ) ;
#8714=EDGE_CURVE ( 'NONE', #4170, #17591, #577, .T. ) ;
#8727=ORIENTED_EDGE ( 'NONE', *, *, #18702, .F. ) ;
#8738=CONICAL_SURFACE ( 'NONE', #6305, 4.000000000000000000, 0.8911886515913786111 ) ;
#8783=CYLINDRICAL_SURFACE ( 'NONE', #5455, 2.500000000000000444 ) ;
#8800=CARTESIAN_POINT ( 'NONE',  ( -0.3208286057739654917, 4.433571671609680465, -0.3503314178412548774 ) ) ;
#8840=DIRECTION ( 'NONE',  ( -0.000000000000000000, 0.000000000000000000, -1.000000000000000000 ) ) ;
#8849=CIRCLE ( 'NONE', #15548, 4.000000000000000000 ) ;
#8878=ADVANCED_FACE ( 'NONE', ( #8922 ), #11697, .T. ) ;
#8882=CARTESIAN_POINT ( 'NONE',  ( -2.059999999999998721, 2.522772406243545965E-16, -0.3080913168122742518 ) ) ;
#8888=CARTESIAN_POINT ( 'NONE',  ( -6.259644161404860030E-16, -4.618802153517027165, -3.433295621305388234 ) ) ;
#8910=EDGE_LOOP ( 'NONE', ( #13124, #12837, #8686, #12057 ) ) ;
#8922=FACE_OUTER_BOUND ( 'NONE', #8365, .T. ) ;
#8982=EDGE_CURVE ( 'NONE', #12688, #15712, #18059, .T. ) ;
#9003=B_SPLINE_CURVE_WITH_KNOTS ( 'NONE', 3,
 ( #157, #3299, #11776, #4820, #1951, #13118 ),
 .UNSPECIFIED., .F., .F.,
 ( 4, 2, 4 ),
 ( 0.002365888236227995517, 0.003551327329835084114, 0.004736766423442172712 ),
 .UNSPECIFIED. ) ;
#9027=CARTESIAN_POINT ( 'NONE',  ( -4.203833317240879275, -1.627343821129593859, -3.597273115243890818 ) ) ;
#9127=DIRECTION ( 'NONE',  ( 0.000000000000000000, 0.000000000000000000, -1.000000000000000000 ) ) ;
#9149=DIRECTION ( 'NONE',  ( 1.000000000000000000, 0.000000000000000000, 0.000000000000000000 ) ) ;
#9156=ORIENTED_EDGE ( 'NONE', *, *, #714, .T. ) ;
#9172=ADVANCED_FACE ( 'NONE', ( #9256 ), #3035, .T. ) ;
#9184=PLANE ( 'NONE',  #1092 ) ;
#9188=CARTESIAN_POINT ( 'NONE',  ( 1.317756351988342622, -3.857995168970215438, -0.04852650426602527628 ) ) ;
#9193=ORIENTED_EDGE ( 'NONE', *, *, #12800, .T. ) ;
#9195=CARTESIAN_POINT ( 'NONE',  ( -0.5276280594146446346, 4.314175951381965746, -3.320322319201721495 ) ) ;
#9200=ORIENTED_EDGE ( 'NONE', *, *, #17985, .T. ) ;
#9229=B_SPLINE_CURVE_WITH_KNOTS ( 'NONE', 3,
 ( #11939, #4895, #1750, #7564, #6222, #17750, #6323, #4698 ),
 .UNSPECIFIED., .F., .F.,
 ( 4, 2, 2, 4 ),
 ( 7.780516681398759253E-20, 0.002450665683189819696, 0.003675998524784729327, 0.004901331366379639391 ),
 .UNSPECIFIED. ) ;
#9244=CARTESIAN_POINT ( 'NONE',  ( -4.198928548860774157, 0.8158838809860065044, -3.526471437616918170 ) ) ;
#9249=ORIENTED_EDGE ( 'NONE', *, *, #4388, .T. ) ;
#9256=FACE_OUTER_BOUND ( 'NONE', #14855, .T. ) ;
#9297=CIRCLE ( 'NONE', #1686, 2.500000000000000888 ) ;
#9298=CARTESIAN_POINT ( 'NONE',  ( 4.175648173966055587, -2.207990556236547608, -3.469390959564065291 ) ) ;
#9301=CARTESIAN_POINT ( 'NONE',  ( 2.756197834950227410, 3.027510591568626896, -3.223146290109805356 ) ) ;
#9323=VERTEX_POINT ( 'NONE', #3482 ) ;
#9354=EDGE_CURVE ( 'NONE', #7704, #15596, #626, .T. ) ;
#9363=CARTESIAN_POINT ( 'NONE',  ( 0.000000000000000000, 0.000000000000000000, 0.000000000000000000 ) ) ;
#9407=DIRECTION ( 'NONE',  ( 1.224646799147353207E-16, 1.000000000000000000, 0.000000000000000000 ) ) ;
#9415=CARTESIAN_POINT ( 'NONE',  ( -1.828356344711647319, -3.563200125723192002, -1.076197711133951296E-14 ) ) ;
#9418=ORIENTED_EDGE ( 'NONE', *, *, #12852, .F. ) ;
#9423=EDGE_CURVE ( 'NONE', #11781, #9323, #9464, .T. ) ;
#9462=CARTESIAN_POINT ( 'NONE',  ( -2.682243648011671588, -3.070208061305317759, -0.04852650426602272971 ) ) ;
#9464=B_SPLINE_CURVE_WITH_KNOTS ( 'NONE', 3,
 ( #15571, #7084, #6899, #15480, #5660, #5484 ),
 .UNSPECIFIED., .F., .F.,
 ( 4, 2, 4 ),
 ( 0.002452478801916361129, 0.003676905084148001344, 0.004901331366379641126 ),
 .UNSPECIFIED. ) ;
#9551=DIRECTION ( 'NONE',  ( 0.000000000000000000, 0.000000000000000000, 1.000000000000000000 ) ) ;
#9567=CARTESIAN_POINT ( 'NONE',  ( 1.734723475976807094E-15, 4.618802153517012954, -0.4999999999999995559 ) ) ;
#9592=EDGE_CURVE ( 'NONE', #104, #2993, #16964, .T. ) ;
#9614=CARTESIAN_POINT ( 'NONE',  ( 4.000000000000000000, 0.000000000000000000, 0.000000000000000000 ) ) ;
#9633=ORIENTED_EDGE ( 'NONE', *, *, #17508, .T. ) ;
#9688=CARTESIAN_POINT ( 'NONE',  ( -6.259644161404860030E-16, -4.618802153517027165, -3.433295621305388234 ) ) ;
#9691=CARTESIAN_POINT ( 'NONE',  ( 0.5636800770130377947, 4.293361309317166530, -3.531542292954102713 ) ) ;
#9753=B_SPLINE_CURVE_WITH_KNOTS ( 'NONE', 3,
 ( #16494, #10675, #9244, #6016, #13364, #127 ),
 .UNSPECIFIED., .F., .F.,
 ( 4, 2, 4 ),
 ( 0.002452478801916376308, 0.003676905084148007850, 0.004901331366379639391 ),
 .UNSPECIFIED. ) ;
#9804=PRODUCT ( 'hex flange nut gradea_iso_ISO - 4161 - M5 - N', 'hex flange nut gradea_iso_ISO - 4161 - M5 - N', '', ( #7352 ) ) ;
#9809=DIRECTION ( 'NONE',  ( -1.000000000000000000, 0.000000000000000000, 0.000000000000000000 ) ) ;
#9816=CARTESIAN_POINT ( 'NONE',  ( -1.390230914382372118, -4.043987460488664532, -3.502507215260523665 ) ) ;
#9818=EDGE_CURVE ( 'NONE', #11704, #1353, #5635, .T. ) ;
#9821=FACE_OUTER_BOUND ( 'NONE', #12422, .T. ) ;
#9846=PLANE ( 'NONE',  #14184 ) ;
#9861=CARTESIAN_POINT ( 'NONE',  ( -4.000000000000000000, 2.309401076758498483, -3.433295621305379353 ) ) ;
#9873=MECHANICAL_DESIGN_GEOMETRIC_PRESENTATION_REPRESENTATION('',(#15961),#14734);
#9900=( LENGTH_UNIT ( ) NAMED_UNIT ( * ) SI_UNIT ( .MILLI., .METRE. ) );
#9906=CARTESIAN_POINT ( 'NONE',  ( 0.1410422978106145031, -4.700232962125109104, -3.687027686973628704 ) ) ;
#9931=ORIENTED_EDGE ( 'NONE', *, *, #8091, .T. ) ;
#9934=DIRECTION ( 'NONE',  ( 1.000000000000000000, 0.000000000000000000, 0.000000000000000000 ) ) ;
#9935=DIRECTION ( 'NONE',  ( 1.000000000000000000, 0.000000000000000000, 0.000000000000000000 ) ) ;
#9938=CIRCLE ( 'NONE', #16927, 2.100000000000000089 ) ;
#9961=ORIENTED_EDGE ( 'NONE', *, *, #4574, .T. ) ;
#9970=ORIENTED_EDGE ( 'NONE', *, *, #18570, .T. ) ;
#9983=ORIENTED_EDGE ( 'NONE', *, *, #8982, .F. ) ;
#9986=ORIENTED_EDGE ( 'NONE', *, *, #8496, .T. ) ;
#10024=CARTESIAN_POINT ( 'NONE',  ( 4.000000000000000000, 0.3987449864460005378, -0.01220643443059817035 ) ) ;
#10025=CARTESIAN_POINT ( 'NONE',  ( 4.000000000000000000, -2.309401076758516691, -0.4999999999999995559 ) ) ;
#10043=VECTOR ( 'NONE', #5187, 1000.000000000000000 ) ;
#10044=DIRECTION ( 'NONE',  ( 1.000000000000000000, 0.000000000000000000, 0.000000000000000000 ) ) ;
#10055=EDGE_CURVE ( 'NONE', #2269, #7704, #6968, .T. ) ;
#10059=FILL_AREA_STYLE_COLOUR ( '', #12296 ) ;
#10081=ORIENTED_EDGE ( 'NONE', *, *, #3033, .F. ) ;
#10093=B_SPLINE_CURVE_WITH_KNOTS ( 'NONE', 3,
 ( #14909, #4615, #6135, #7742, #17755, #15000, #11946, #7570 ),
 .UNSPECIFIED., .F., .F.,
 ( 4, 2, 2, 4 ),
 ( 2.465131517071352357E-07, 0.001183067374689843057, 0.001774477805458910071, 0.002365888236227977302 ),
 .UNSPECIFIED. ) ;
#10121=ORIENTED_EDGE ( 'NONE', *, *, #16059, .T. ) ;
#10162=EDGE_CURVE ( 'NONE', #11921, #2367, #6928, .T. ) ;
#10174=EDGE_CURVE ( 'NONE', #4891, #14252, #8849, .T. ) ;
#10181=CARTESIAN_POINT ( 'NONE',  ( -4.197312064133472020, -0.8182229787990021874, -3.502518405183886685 ) ) ;
#10285=EDGE_LOOP ( 'NONE', ( #10121, #11645, #14908 ) ) ;
#10300=DIRECTION ( 'NONE',  ( 1.000000000000000000, 0.000000000000000000, 0.000000000000000000 ) ) ;
#10344=CARTESIAN_POINT ( 'NONE',  ( 0.5276280594147412240, -4.314175951381924889, -3.320322319201654881 ) ) ;
#10353=CARTESIAN_POINT ( 'NONE',  ( -6.473970235329672780E-16, -4.862606272033106691, -3.745885042887442395 ) ) ;
#10360=EDGE_CURVE ( 'NONE', #14252, #13512, #9003, .T. ) ;
#10371=CARTESIAN_POINT ( 'NONE',  ( 2.171643655288379993, -3.365003104552334978, -1.195831703456429434E-14 ) ) ;
#10391=EDGE_CURVE ( 'NONE', #16921, #15596, #12425, .T. ) ;
#10415=DIRECTION ( 'NONE',  ( 1.000000000000000000, 0.000000000000000000, 0.000000000000000000 ) ) ;
#10423=EDGE_CURVE ( 'NONE', #2818, #104, #18324, .T. ) ;
#10428=CARTESIAN_POINT ( 'NONE',  ( -2.000000000000007550, -3.464101615137749945, 0.000000000000000000 ) ) ;
#10445=CARTESIAN_POINT ( 'NONE',  ( 2.725741868436127202, -3.045094352033990148, -3.220599429844051453 ) ) ;
#10478=B_SPLINE_CURVE_WITH_KNOTS ( 'NONE', 3,
 ( #8888, #12023, #17662, #1935, #4892 ),
 .UNSPECIFIED., .F., .F.,
 ( 4, 1, 4 ),
 ( 5.640274452250024914E-20, 0.002309401076758505356, 0.004618802153517010713 ),
 .UNSPECIFIED. ) ;
#10496=ADVANCED_FACE ( 'NONE', ( #10990 ), #4909, .T. ) ;
#10590=AXIS2_PLACEMENT_3D ( 'NONE', #8597, #6991, #9935 ) ;
#10655=CARTESIAN_POINT ( 'NONE',  ( 4.203833317240879275, 1.627343821129582979, -3.597273115243889929 ) ) ;
#10658=B_SPLINE_CURVE_WITH_KNOTS ( 'NONE', 3,
 ( #13259, #14773, #11835, #1728, #12107 ),
 .UNSPECIFIED., .F., .F.,
 ( 4, 1, 4 ),
 ( 0.000000000000000000, 0.002309401076758506657, 0.004618802153517013315 ),
 .UNSPECIFIED. ) ;
#10675=CARTESIAN_POINT ( 'NONE',  ( -4.197393957002303999, 0.4069871074557429025, -3.503767560748926257 ) ) ;
#10683=CARTESIAN_POINT ( 'NONE',  ( -2.688821387764050996E-14, -4.618802153517012954, -0.4999999999999995559 ) ) ;
#10692=ORIENTED_EDGE ( 'NONE', *, *, #15521, .T. ) ;
#10708=DIRECTION ( 'NONE',  ( 0.000000000000000000, 0.000000000000000000, -1.000000000000000000 ) ) ;
#10711=VERTEX_POINT ( 'NONE', #1562 ) ;
#10715=ORIENTED_EDGE ( 'NONE', *, *, #16992, .F. ) ;
#10730=ORIENTED_EDGE ( 'NONE', *, *, #5274, .T. ) ;
#10745=DIRECTION ( 'NONE',  ( -0.000000000000000000, -0.000000000000000000, 1.000000000000000000 ) ) ;
#10805=CARTESIAN_POINT ( 'NONE',  ( 1.312671235360372224, 3.860931062424219462, -0.05923475698270440348 ) ) ;
#10820=CARTESIAN_POINT ( 'NONE',  ( 1.390230914382191596, 4.043987460488659202, -3.502507215260488582 ) ) ;
#10824=VERTEX_POINT ( 'NONE', #14896 ) ;
#10829=CARTESIAN_POINT ( 'NONE',  ( -2.000000000000007550, -3.464101615137749945, 0.000000000000000000 ) ) ;
#10842=ORIENTED_EDGE ( 'NONE', *, *, #10423, .T. ) ;
#10852=CARTESIAN_POINT ( 'NONE',  ( -4.175002511812151873, -2.208363329454905877, -3.469254087858246738 ) ) ;
#10891=CARTESIAN_POINT ( 'NONE',  ( -1.393927851585477606, 4.043713361053528743, -3.526374918436835149 ) ) ;
#10899=CARTESIAN_POINT ( 'NONE',  ( -2.100000000000000089, 2.571758278209441957E-16, -0.2800830152838844622 ) ) ;
#10930=AXIS2_PLACEMENT_3D ( 'NONE', #5255, #12301, #3462 ) ;
#10943=ORIENTED_EDGE ( 'NONE', *, *, #1334, .T. ) ;
#10990=FACE_OUTER_BOUND ( 'NONE', #17138, .T. ) ;
#11017=CARTESIAN_POINT ( 'NONE',  ( 0.000000000000000000, 0.000000000000000000, -0.3080913168122742518 ) ) ;
#11022=ORIENTED_EDGE ( 'NONE', *, *, #9423, .F. ) ;
#11041=FACE_OUTER_BOUND ( 'NONE', #8249, .T. ) ;
#11057=AXIS2_PLACEMENT_3D ( 'NONE', #12704, #5175, #13943 ) ;
#11090=ORIENTED_EDGE ( 'NONE', *, *, #18422, .F. ) ;
#11097=EDGE_CURVE ( 'NONE', #12396, #13512, #12375, .T. ) ;
#11105=PLANE ( 'NONE',  #3260 ) ;
#11108=CARTESIAN_POINT ( 'NONE',  ( -0.6666666666666666297, -4.233901974057276973, -3.300726591567087365 ) ) ;
#11112=CARTESIAN_POINT ( 'NONE',  ( 0.000000000000000000, 0.000000000000000000, 0.000000000000000000 ) ) ;
#11119=ORIENTED_EDGE ( 'NONE', *, *, #5319, .F. ) ;
#11120=ORIENTED_EDGE ( 'NONE', *, *, #9354, .F. ) ;
#11126=EDGE_CURVE ( 'NONE', #10711, #15712, #2876, .T. ) ;
#11142=CARTESIAN_POINT ( 'NONE',  ( 0.1756481739660539498, -4.720212674038995360, -3.469390959564070620 ) ) ;
#11157=CIRCLE ( 'NONE', #13010, 4.000000000000000000 ) ;
#11174=FACE_OUTER_BOUND ( 'NONE', #4417, .T. ) ;
#11263=CARTESIAN_POINT ( 'NONE',  ( 4.000000000000000000, 0.000000000000000000, 0.000000000000000000 ) ) ;
#11268=CARTESIAN_POINT ( 'NONE',  ( 4.000000000000000000, 0.000000000000000000, 0.000000000000000000 ) ) ;
#11299=DIRECTION ( 'NONE',  ( 0.000000000000000000, 0.000000000000000000, 1.000000000000000000 ) ) ;
#11308=DIRECTION ( 'NONE',  ( 0.000000000000000000, 0.000000000000000000, -1.000000000000000000 ) ) ;
#11449=CARTESIAN_POINT ( 'NONE',  ( 4.000000000000000000, 0.1981133338132474442, 2.382280164152719704E-17 ) ) ;
#11450=EDGE_CURVE ( 'NONE', #11921, #12688, #2648, .T. ) ;
#11458=( GEOMETRIC_REPRESENTATION_CONTEXT ( 3 ) GLOBAL_UNCERTAINTY_ASSIGNED_CONTEXT ( ( #15111 ) ) GLOBAL_UNIT_ASSIGNED_CONTEXT ( ( #16276, #13431, #12185 ) ) REPRESENTATION_CONTEXT ( 'NONE', 'WORKASPACE' ) );
#11466=B_SPLINE_CURVE_WITH_KNOTS ( 'NONE', 3,
 ( #2136, #7941, #525, #18234, #10891, #8137, #12421, #5182 ),
 .UNSPECIFIED., .F., .F.,
 ( 4, 2, 2, 4 ),
 ( 0.000000000000000000, 0.002450665683189820997, 0.003675998524784731495, 0.004901331366379641993 ),
 .UNSPECIFIED. ) ;
#11483=VERTEX_POINT ( 'NONE', #2565 ) ;
#11501=CARTESIAN_POINT ( 'NONE',  ( 2.500000000000000888, 3.061616997868384127E-16, -4.974599999999998801 ) ) ;
#11518=CARTESIAN_POINT ( 'NONE',  ( -4.000000000000000000, -2.309401076758512694, -3.433295621305382461 ) ) ;
#11532=CARTESIAN_POINT ( 'NONE',  ( -4.000000000000000000, -2.472261339043343220, -3.687027428081192326 ) ) ;
#11553=CARTESIAN_POINT ( 'NONE',  ( -2.500000000000000444, 3.061616997868383634E-16, -25.03750572909317285 ) ) ;
#11581=CARTESIAN_POINT ( 'NONE',  ( 0.000000000000000000, 0.000000000000000000, -0.3080913168122742518 ) ) ;
#11582=ADVANCED_FACE ( 'NONE', ( #16862 ), #3623, .F. ) ;
#11589=( NAMED_UNIT ( * ) PLANE_ANGLE_UNIT ( ) SI_UNIT ( $, .RADIAN. ) );
#11645=ORIENTED_EDGE ( 'NONE', *, *, #3376, .T. ) ;
#11647=DIRECTION ( 'NONE',  ( -0.000000000000000000, -0.000000000000000000, 1.000000000000000000 ) ) ;
#11697=PLANE ( 'NONE',  #12450 ) ;
#11704=VERTEX_POINT ( 'NONE', #7890 ) ;
#11744=AXIS2_PLACEMENT_3D ( 'NONE', #1197, #2997, #10044 ) ;
#11747=CARTESIAN_POINT ( 'NONE',  ( 4.211140560182196957, 2.431303136016536470, -3.745885042887433514 ) ) ;
#11773=CARTESIAN_POINT ( 'NONE',  ( -0.1404048886732797152, -4.699864953788083888, -3.686887068327043160 ) ) ;
#11776=CARTESIAN_POINT ( 'NONE',  ( 2.682243648011666703, 3.070208061305304881, -0.04852650426601266831 ) ) ;
#11781=VERTEX_POINT ( 'NONE', #14849 ) ;
#11788=DIRECTION ( 'NONE',  ( 0.000000000000000000, 0.000000000000000000, -1.000000000000000000 ) ) ;
#11792=EDGE_CURVE ( 'NONE', #10824, #11956, #6018, .T. ) ;
#11803=CARTESIAN_POINT ( 'NONE',  ( 0.000000000000000000, 0.000000000000000000, 0.000000000000000000 ) ) ;
#11805=CARTESIAN_POINT ( 'NONE',  ( -4.000000000000000000, -1.680117682357936904, -3.316611593218794951 ) ) ;
#11835=CARTESIAN_POINT ( 'NONE',  ( -1.999999999999999556, 3.464101615137754830, -3.142992957459232795 ) ) ;
#11837=ORIENTED_EDGE ( 'NONE', *, *, #8496, .F. ) ;
#11841=CARTESIAN_POINT ( 'NONE',  ( 4.101954839143203912, 2.368264730583012234, -3.681130640444374436 ) ) ;
#11846=CARTESIAN_POINT ( 'NONE',  ( 5.560781378645573980, 6.809993116116507654E-16, -4.000000000000000000 ) ) ;
#11863=FACE_OUTER_BOUND ( 'NONE', #4650, .T. ) ;
#11866=CARTESIAN_POINT ( 'NONE',  ( 0.3208286057739604957, -4.433571671609698228, -0.3503314178412692548 ) ) ;
#11867=EDGE_LOOP ( 'NONE', ( #2815, #10943, #7561, #1889, #5963, #14559, #9970 ) ) ;
#11877=VERTEX_POINT ( 'NONE', #3894 ) ;
#11890=CARTESIAN_POINT ( 'NONE',  ( -2.688821387764050996E-14, -4.618802153517012954, -0.4999999999999995559 ) ) ;
#11901=ADVANCED_FACE ( 'NONE', ( #16752 ), #2341, .F. ) ;
#11906=EDGE_LOOP ( 'NONE', ( #16186, #12444, #13980, #1799 ) ) ;
#11921=VERTEX_POINT ( 'NONE', #12551 ) ;
#11939=CARTESIAN_POINT ( 'NONE',  ( 1.411581201560190495E-15, 4.862606272033091592, -3.745885042887436622 ) ) ;
#11944=CLOSED_SHELL ( 'NONE', ( #18783, #3886, #11901, #16124, #3308, #7828, #14825, #4660, #8878, #2239, #13556, #14932, #4533, #13769, #988, #1096, #13262, #8197, #5421, #16954, #10496, #5524, #9172, #6832, #13307, #11582, #15984, #18073, #1263, #3195, #15711, #6564 ) ) ;
#11946=CARTESIAN_POINT ( 'NONE',  ( -2.171643655288372443, 3.365003104552320767, 2.541098841762897165E-18 ) ) ;
#11953=FACE_OUTER_BOUND ( 'NONE', #8529, .T. ) ;
#11956=VERTEX_POINT ( 'NONE', #5214 ) ;
#11962=CARTESIAN_POINT ( 'NONE',  ( -1.257172072275743346, 3.892973519171203378, -3.433252694550776862 ) ) ;
#12007=CONICAL_SURFACE ( 'NONE', #14148, 5.560781378645573980, 1.221730476396046816 ) ;
#12013=EDGE_CURVE ( 'NONE', #104, #11956, #802, .T. ) ;
#12014=EDGE_CURVE ( 'NONE', #7161, #2269, #7606, .T. ) ;
#12023=CARTESIAN_POINT ( 'NONE',  ( 0.6666666666666658525, -4.233901974057276085, -3.300726591567086476 ) ) ;
#12036=EDGE_LOOP ( 'NONE', ( #16622, #5964 ) ) ;
#12038=CONICAL_SURFACE ( 'NONE', #16302, 2.059999999999998721, 0.9599310885968738161 ) ;
#12054=CARTESIAN_POINT ( 'NONE',  ( -4.141042297810615835, 2.227970268150415656, -3.687027686973619822 ) ) ;
#12057=ORIENTED_EDGE ( 'NONE', *, *, #780, .F. ) ;
#12107=CARTESIAN_POINT ( 'NONE',  ( -4.000000000000000000, 2.309401076758498483, -3.433295621305379353 ) ) ;
#12169=CARTESIAN_POINT ( 'NONE',  ( -4.101948962586059011, 2.368261337751163875, -3.681124513963739187 ) ) ;
#12172=APPLICATION_CONTEXT ( 'automotive_design' ) ;
#12185=( NAMED_UNIT ( * ) SI_UNIT ( $, .STERADIAN. ) SOLID_ANGLE_UNIT ( ) );
#12193=DIRECTION ( 'NONE',  ( -1.000000000000000000, 0.000000000000000000, 0.000000000000000000 ) ) ;
#12243=PRODUCT_DEFINITION ( 'UNKNOWN', '', #5004, #16068 ) ;
#12245=CARTESIAN_POINT ( 'NONE',  ( -3.436319922987618902, 2.634841920961291439, -3.531542292955721862 ) ) ;
#12282=CARTESIAN_POINT ( 'NONE',  ( 4.000000000000000000, 2.512223110932545023, -3.469391141908803711 ) ) ;
#12286=CARTESIAN_POINT ( 'NONE',  ( 5.384454397937118664, 0.000000000000000000, -4.484454397937119197 ) ) ;
#12291=CARTESIAN_POINT ( 'NONE',  ( -4.000000000000000000, -1.942223658245633811, -0.3516579909967644246 ) ) ;
#12296=COLOUR_RGB ( '',1.000000000000000000, 0.9490196078431372140, 0.9098039215686274384 ) ;
#12301=DIRECTION ( 'NONE',  ( 0.000000000000000000, 0.000000000000000000, -1.000000000000000000 ) ) ;
#12320=B_SPLINE_CURVE_WITH_KNOTS ( 'NONE', 3,
 ( #12872, #8296, #14096, #8485, #7133, #16865 ),
 .UNSPECIFIED., .F., .F.,
 ( 4, 2, 4 ),
 ( 4.336808689942017736E-19, 0.0002095117440864781224, 0.0004190234881729558111 ),
 .UNSPECIFIED. ) ;
#12333=ORIENTED_EDGE ( 'NONE', *, *, #7870, .F. ) ;
#12375=B_SPLINE_CURVE_WITH_KNOTS ( 'NONE', 3,
 ( #11263, #11449, #10024, #17086, #2786, #15641, #12590, #8587 ),
 .UNSPECIFIED., .F., .F.,
 ( 4, 2, 2, 4 ),
 ( 0.005725059856848645212, 0.006314084072593634418, 0.006903108288338624492, 0.008081156719828603771 ),
 .UNSPECIFIED. ) ;
#12388=CARTESIAN_POINT ( 'NONE',  ( -2.756197834950067094, -3.027510591568735254, -3.223146290109809797 ) ) ;
#12391=ORIENTED_EDGE ( 'NONE', *, *, #17963, .T. ) ;
#12396=VERTEX_POINT ( 'NONE', #11268 ) ;
#12417=ORIENTED_EDGE ( 'NONE', *, *, #5319, .T. ) ;
#12421=CARTESIAN_POINT ( 'NONE',  ( -0.3461262719736137305, 4.658553426539289610, -3.671615880910373608 ) ) ;
#12422=EDGE_LOOP ( 'NONE', ( #10730, #290, #3023 ) ) ;
#12425=B_SPLINE_CURVE_WITH_KNOTS ( 'NONE', 3,
 ( #251, #3391, #9188, #6056, #11866, #17678 ),
 .UNSPECIFIED., .F., .F.,
 ( 4, 2, 4 ),
 ( 0.002365888236227967761, 0.003551327329835077609, 0.004736766423442186590 ),
 .UNSPECIFIED. ) ;
#12444=ORIENTED_EDGE ( 'NONE', *, *, #11450, .F. ) ;
#12450=AXIS2_PLACEMENT_3D ( 'NONE', #4367, #4452, #6533 ) ;
#12479=FACE_OUTER_BOUND ( 'NONE', #12036, .T. ) ;
#12486=CARTESIAN_POINT ( 'NONE',  ( -3.472371940586054251, -2.614027278893156669, -3.320322319202162031 ) ) ;
#12497=DIRECTION ( 'NONE',  ( 0.8191520442889875797, 0.000000000000000000, 0.5735764363510522656 ) ) ;
#12531=DIRECTION ( 'NONE',  ( 1.000000000000000000, 0.000000000000000000, 0.000000000000000000 ) ) ;
#12551=CARTESIAN_POINT ( 'NONE',  ( 2.100000000000000089, 0.000000000000000000, -4.694516984716113228 ) ) ;
#12590=CARTESIAN_POINT ( 'NONE',  ( 3.999999999999999112, 1.941961291383486277, -0.3515519931180248192 ) ) ;
#12591=CARTESIAN_POINT ( 'NONE',  ( -5.384454397937118664, 6.702023979852544604E-16, -5.000000000000000000 ) ) ;
#12598=CYLINDRICAL_SURFACE ( 'NONE', #2548, 2.500000000000000444 ) ;
#12639=VERTEX_POINT ( 'NONE', #3445 ) ;
#12640=CARTESIAN_POINT ( 'NONE',  ( -3.333333333333332149, -2.694301256218264218, -3.300726591567082036 ) ) ;
#12668=CARTESIAN_POINT ( 'NONE',  ( -6.473970235329672780E-16, -4.862606272033106691, -3.745885042887442395 ) ) ;
#12683=AXIS2_PLACEMENT_3D ( 'NONE', #2104, #7909, #9809 ) ;
#12685=AXIS2_PLACEMENT_3D ( 'NONE', #7882, #7425, #10300 ) ;
#12687=EDGE_CURVE ( 'NONE', #7169, #17591, #2295, .T. ) ;
#12688=VERTEX_POINT ( 'NONE', #8102 ) ;
#12689=ORIENTED_EDGE ( 'NONE', *, *, #12014, .F. ) ;
#12704=CARTESIAN_POINT ( 'NONE',  ( 0.000000000000000000, 0.000000000000000000, 0.000000000000000000 ) ) ;
#12711=AXIS2_PLACEMENT_3D ( 'NONE', #11112, #11308, #8358 ) ;
#12719=DIRECTION ( 'NONE',  ( 1.000000000000000000, 0.000000000000000000, 0.000000000000000000 ) ) ;
#12721=EDGE_CURVE ( 'NONE', #15712, #2367, #9297, .T. ) ;
#12723=DIRECTION ( 'NONE',  ( -0.000000000000000000, -0.000000000000000000, 1.000000000000000000 ) ) ;
#12743=DIRECTION ( 'NONE',  ( 0.8191520442889902442, 1.003171929053522651E-16, -0.5735764363510482688 ) ) ;
#12800=EDGE_CURVE ( 'NONE', #2367, #15712, #14434, .T. ) ;
#12801=CARTESIAN_POINT ( 'NONE',  ( 0.000000000000000000, 0.000000000000000000, 0.000000000000000000 ) ) ;
#12809=VECTOR ( 'NONE', #12743, 1000.000000000000114 ) ;
#12816=DIRECTION ( 'NONE',  ( -0.000000000000000000, -0.000000000000000000, 1.000000000000000000 ) ) ;
#12837=ORIENTED_EDGE ( 'NONE', *, *, #7937, .F. ) ;
#12839=CARTESIAN_POINT ( 'NONE',  ( -1.655952806101422814, 3.662737355149034979, -7.623296525288699970E-18 ) ) ;
#12842=ORIENTED_EDGE ( 'NONE', *, *, #10391, .T. ) ;
#12852=EDGE_CURVE ( 'NONE', #2818, #9323, #12320, .T. ) ;
#12857=DIRECTION ( 'NONE',  ( -1.000000000000000000, 0.000000000000000000, 0.000000000000000000 ) ) ;
#12872=CARTESIAN_POINT ( 'NONE',  ( 4.000000000000000000, -2.309401076758514915, -3.433295621305383349 ) ) ;
#12892=DIRECTION ( 'NONE',  ( 1.000000000000000000, 0.000000000000000000, 0.000000000000000000 ) ) ;
#12897=VECTOR ( 'NONE', #7286, 1000.000000000000000 ) ;
#12898=DIRECTION ( 'NONE',  ( 1.000000000000000000, 0.000000000000000000, 0.000000000000000000 ) ) ;
#12917=SURFACE_STYLE_FILL_AREA ( #6046 ) ;
#12949=CARTESIAN_POINT ( 'NONE',  ( 0.000000000000000000, 0.000000000000000000, -4.000000000000000000 ) ) ;
#12958=CARTESIAN_POINT ( 'NONE',  ( 0.02511973781850649831, -4.877415612947427981, -3.751298745799844792 ) ) ;
#13010=AXIS2_PLACEMENT_3D ( 'NONE', #11803, #8840, #14655 ) ;
#13053=CIRCLE ( 'NONE', #5442, 2.100000000000000089 ) ;
#13070=EDGE_CURVE ( 'NONE', #15596, #13860, #5271, .T. ) ;
#13104=EDGE_CURVE ( 'NONE', #2993, #11781, #6184, .T. ) ;
#13118=CARTESIAN_POINT ( 'NONE',  ( 4.000000000000000000, 2.309401076758515803, -0.4999999999999995559 ) ) ;
#13124=ORIENTED_EDGE ( 'NONE', *, *, #13318, .T. ) ;
#13133=AXIS2_PLACEMENT_3D ( 'NONE', #2148, #10708, #5280 ) ;
#13143=CARTESIAN_POINT ( 'NONE',  ( -4.000000000000000000, 2.471528634177585282, -3.686887442155186712 ) ) ;
#13151=AXIS2_PLACEMENT_3D ( 'NONE', #1, #18749, #12857 ) ;
#13188=DIRECTION ( 'NONE',  ( -0.000000000000000000, -0.000000000000000000, 1.000000000000000000 ) ) ;
#13191=ORIENTED_EDGE ( 'NONE', *, *, #12013, .F. ) ;
#13201=DIRECTION ( 'NONE',  ( 0.000000000000000000, 0.000000000000000000, -1.000000000000000000 ) ) ;
#13208=ORIENTED_EDGE ( 'NONE', *, *, #14036, .F. ) ;
#13214=ORIENTED_EDGE ( 'NONE', *, *, #12687, .T. ) ;
#13243=EDGE_LOOP ( 'NONE', ( #16071, #1832, #13214, #16668 ) ) ;
#13248=CARTESIAN_POINT ( 'NONE',  ( -6.259644161404860030E-16, -4.618802153517027165, -3.433295621305388234 ) ) ;
#13259=CARTESIAN_POINT ( 'NONE',  ( 1.567478505476134606E-15, 4.618802153517012066, -3.433295621305382905 ) ) ;
#13262=ADVANCED_FACE ( 'NONE', ( #11953 ), #12007, .T. ) ;
#13296=CARTESIAN_POINT ( 'NONE',  ( 1.360585162435110629, -4.061296242128317857, -3.505054077164905024 ) ) ;
#13307=ADVANCED_FACE ( 'NONE', ( #11863 ), #13350, .F. ) ;
#13318=EDGE_CURVE ( 'NONE', #16201, #7161, #2785, .T. ) ;
#13321=CARTESIAN_POINT ( 'NONE',  ( 3.522875095019493141, -2.820352903225631369, -3.598441714920572299 ) ) ;
#13332=CARTESIAN_POINT ( 'NONE',  ( -3.999999999998910649, -1.658469974638591804, -3.531532913075256186 ) ) ;
#13347=AXIS2_PLACEMENT_3D ( 'NONE', #3813, #15436, #2387 ) ;
#13350=( BOUNDED_SURFACE ( )  B_SPLINE_SURFACE ( 3, 2, ( 
 ( #1858, #11773, #7661 ),
 ( #10344, #16155, #17675 ),
 ( #14718, #1667, #13296 ),
 ( #10445, #3499, #7774 ),
 ( #13602, #13697, #13321 ),
 ( #9298, #16457, #552 ) ),
 .UNSPECIFIED., .F., .F., .F. ) 
 B_SPLINE_SURFACE_WITH_KNOTS ( ( 4, 2, 4 ),
 ( 3, 3 ),
 ( 0.02032853247518126918, 0.02278863295364821906, 0.02524873343211517240 ),
 ( 0.000000000000000000, 1.000000000000000000 ),
 .UNSPECIFIED. ) 
 GEOMETRIC_REPRESENTATION_ITEM ( )  RATIONAL_B_SPLINE_SURFACE ( (
 ( 1.000000000000000000, 0.8047781615896837382, 1.000000000000000000),
 ( 1.000000000000000000, 0.8123767586289252218, 1.000000000000000000),
 ( 1.000000000000000000, 0.8190662415564388121, 1.000000000000000000),
 ( 1.000000000000000000, 0.8192361015669026303, 1.000000000000000000),
 ( 1.000000000000000000, 0.8126135807103900266, 1.000000000000000000),
 ( 1.000000000000000000, 0.8047712338318593339, 1.000000000000000000) ) ) 
 REPRESENTATION_ITEM ( '' )  SURFACE ( )  );
#13355=CARTESIAN_POINT ( 'NONE',  ( -1.149515148933674504E-15, -4.647091401871393579, -3.572172305156879890 ) ) ;
#13364=CARTESIAN_POINT ( 'NONE',  ( -4.207491450040567571, 2.029819825146470524, -3.671670828759566074 ) ) ;
#13408=CARTESIAN_POINT ( 'NONE',  ( -2.725741868435985094, 3.045094352034055429, -3.220599429844047012 ) ) ;
#13421=CARTESIAN_POINT ( 'NONE',  ( -4.000000000000000000, 0.000000000000000000, 0.000000000000000000 ) ) ;
#13426=CARTESIAN_POINT ( 'NONE',  ( 2.000000000000005329, -3.464101615137751722, 0.000000000000000000 ) ) ;
#13431=( NAMED_UNIT ( * ) PLANE_ANGLE_UNIT ( ) SI_UNIT ( $, .RADIAN. ) );
#13487=FACE_OUTER_BOUND ( 'NONE', #16659, .T. ) ;
#13512=VERTEX_POINT ( 'NONE', #6733 ) ;
#13514=CARTESIAN_POINT ( 'NONE',  ( 4.000000000000000000, -2.309401076758516691, -0.4999999999999995559 ) ) ;
#13556=ADVANCED_FACE ( 'NONE', ( #16834 ), #3783, .T. ) ;
#13602=CARTESIAN_POINT ( 'NONE',  ( 3.455068668934414777, -2.624017327439094327, -3.316620875263732504 ) ) ;
#13614=CARTESIAN_POINT ( 'NONE',  ( 1.567478505476134606E-15, 4.618802153517012066, -3.433295621305382905 ) ) ;
#13640=LINE ( 'NONE', #5047, #1769 ) ;
#13697=CARTESIAN_POINT ( 'NONE',  ( 3.436319922986518449, -2.634841920959471562, -3.531542292954761741 ) ) ;
#13704=CARTESIAN_POINT ( 'NONE',  ( 3.453038570460273071, 2.625189405340834448, -3.535263753543585352 ) ) ;
#13722=CARTESIAN_POINT ( 'NONE',  ( 4.000000000000000000, -1.700175430507292473, -3.320327275037661785 ) ) ;
#13727=DIRECTION ( 'NONE',  ( -0.000000000000000000, -0.000000000000000000, 1.000000000000000000 ) ) ;
#13734=ORIENTED_EDGE ( 'NONE', *, *, #17359, .T. ) ;
#13747=EDGE_LOOP ( 'NONE', ( #2180, #12333, #3973, #9193 ) ) ;
#13754=PLANE ( 'NONE',  #1404 ) ;
#13769=ADVANCED_FACE ( 'NONE', ( #1947, #13487 ), #9184, .F. ) ;
#13773=CARTESIAN_POINT ( 'NONE',  ( 0.1750025118121568690, 4.719839900820621104, -3.469254087858248070 ) ) ;
#13813=CARTESIAN_POINT ( 'NONE',  ( -3.540020015735593439, -2.810662092924100630, -3.602146406945814672 ) ) ;
#13860=VERTEX_POINT ( 'NONE', #10428 ) ;
#13885=DIRECTION ( 'NONE',  ( -0.000000000000000000, -0.000000000000000000, 1.000000000000000000 ) ) ;
#13894=TOROIDAL_SURFACE ( 'NONE', #2036, 5.384454397937118664, 0.5155456020628804703 ) ;
#13911=CARTESIAN_POINT ( 'NONE',  ( 4.000000000000000000, -1.942223658245635809, -0.3516579909967643691 ) ) ;
#13912=FACE_OUTER_BOUND ( 'NONE', #13243, .T. ) ;
#13943=DIRECTION ( 'NONE',  ( -1.000000000000000000, 0.000000000000000000, 0.000000000000000000 ) ) ;
#13950=DIRECTION ( 'NONE',  ( 0.000000000000000000, -0.000000000000000000, 1.000000000000000000 ) ) ;
#13980=ORIENTED_EDGE ( 'NONE', *, *, #18676, .T. ) ;
#14004=FACE_BOUND ( 'NONE', #4362, .T. ) ;
#14036=EDGE_CURVE ( 'NONE', #12396, #14252, #14778, .T. ) ;
#14037=CARTESIAN_POINT ( 'NONE',  ( 2.100000000000000089, 0.000000000000000000, -5.000000000000000000 ) ) ;
#14046=B_SPLINE_CURVE_WITH_KNOTS ( 'NONE', 3,
 ( #961, #13911, #6760, #2189, #7996, #9614 ),
 .UNSPECIFIED., .F., .F.,
 ( 4, 2, 4 ),
 ( 0.003358874760055551890, 0.004541967308452098118, 0.005725059856848645212 ),
 .UNSPECIFIED. ) ;
#14053=ORIENTED_EDGE ( 'NONE', *, *, #12800, .F. ) ;
#14055=CARTESIAN_POINT ( 'NONE',  ( 4.211140560182196957, 2.431303136016536470, -3.745885042887433514 ) ) ;
#14071=CARTESIAN_POINT ( 'NONE',  ( -0.1410422978106123659, 4.700232962125094893, -3.687027686973624707 ) ) ;
#14084=ORIENTED_EDGE ( 'NONE', *, *, #714, .F. ) ;
#14096=CARTESIAN_POINT ( 'NONE',  ( 4.024499207728847949, -2.323545700935699454, -3.572172305156873673 ) ) ;
#14120=ORIENTED_EDGE ( 'NONE', *, *, #14693, .F. ) ;
#14148=AXIS2_PLACEMENT_3D ( 'NONE', #14531, #13201, #4433 ) ;
#14184=AXIS2_PLACEMENT_3D ( 'NONE', #15563, #1190, #6891 ) ;
#14252=VERTEX_POINT ( 'NONE', #132 ) ;
#14262=AXIS2_PLACEMENT_3D ( 'NONE', #4607, #17747, #10415 ) ;
#14267=CARTESIAN_POINT ( 'NONE',  ( 0.000000000000000000, 0.000000000000000000, -5.000000000000000000 ) ) ;
#14321=CARTESIAN_POINT ( 'NONE',  ( -4.000000000000000000, 0.9868501483902560878, -0.09357334158579519445 ) ) ;
#14324=DIRECTION ( 'NONE',  ( 0.000000000000000000, 0.000000000000000000, 1.000000000000000000 ) ) ;
#14338=LINE ( 'NONE', #7092, #15317 ) ;
#14368=CARTESIAN_POINT ( 'NONE',  ( 0.000000000000000000, 0.000000000000000000, -4.000000000000000000 ) ) ;
#14387=CARTESIAN_POINT ( 'NONE',  ( -2.742827927723112236, -3.035229711105190464, -3.433252694550595230 ) ) ;
#14434=CIRCLE ( 'NONE', #16928, 2.500000000000000888 ) ;
#14468=CARTESIAN_POINT ( 'NONE',  ( -0.6448876103708541807, -4.246476118072358474, -0.2256878752776773356 ) ) ;
#14469=EDGE_LOOP ( 'NONE', ( #4926, #11022, #17886, #18630, #15098 ) ) ;
#14470=CARTESIAN_POINT ( 'NONE',  ( -2.836893136758495970, -3.208949435745868328, -3.505054077164885484 ) ) ;
#14472=DIRECTION ( 'NONE',  ( 0.000000000000000000, 0.000000000000000000, -1.000000000000000000 ) ) ;
#14503=B_SPLINE_CURVE_WITH_KNOTS ( 'NONE', 3,
 ( #7916, #12291, #18292, #16687, #781, #6582 ),
 .UNSPECIFIED., .F., .F.,
 ( 4, 2, 4 ),
 ( 0.003358874760055550156, 0.004541967308452096383, 0.005725059856848641743 ),
 .UNSPECIFIED. ) ;
#14510=CARTESIAN_POINT ( 'NONE',  ( 4.154306624730864428, 2.398490048084778170, -3.721999068284300272 ) ) ;
#14523=SHAPE_REPRESENTATION_RELATIONSHIP ( 'NONE' , 'NONE' ,  #2517, #17412 ) ;
#14531=CARTESIAN_POINT ( 'NONE',  ( 0.000000000000000000, 0.000000000000000000, -4.000000000000000000 ) ) ;
#14559=ORIENTED_EDGE ( 'NONE', *, *, #780, .T. ) ;
#14608=CARTESIAN_POINT ( 'NONE',  ( 4.000000000000000000, 2.309401076758497151, -3.433295621305379353 ) ) ;
#14638=CARTESIAN_POINT ( 'NONE',  ( 1.747541505913279281, -3.837784562140273081, -3.503702292528912299 ) ) ;
#14655=DIRECTION ( 'NONE',  ( -1.000000000000000000, 0.000000000000000000, 0.000000000000000000 ) ) ;
#14669=EDGE_LOOP ( 'NONE', ( #2742, #15453, #17445, #14053 ) ) ;
#14684=DIRECTION ( 'NONE',  ( 0.000000000000000000, -0.000000000000000000, 1.000000000000000000 ) ) ;
#14693=EDGE_CURVE ( 'NONE', #1353, #3828, #6900, .T. ) ;
#14702=EDGE_LOOP ( 'NONE', ( #18359, #8630, #3343 ) ) ;
#14718=CARTESIAN_POINT ( 'NONE',  ( 1.243802165048773611, -3.900692638707475624, -3.223146290109810241 ) ) ;
#14734=( GEOMETRIC_REPRESENTATION_CONTEXT ( 3 ) GLOBAL_UNCERTAINTY_ASSIGNED_CONTEXT ( ( #6149 ) ) GLOBAL_UNIT_ASSIGNED_CONTEXT ( ( #9900, #11589, #17393 ) ) REPRESENTATION_CONTEXT ( 'NONE', 'WORKASPACE' ) );
#14744=CARTESIAN_POINT ( 'NONE',  ( -4.211405944401398038, -2.460460786169389902, -3.751298493805494072 ) ) ;
#14773=CARTESIAN_POINT ( 'NONE',  ( -0.6666666666666651864, 4.233901974057260098, -3.300726591567081147 ) ) ;
#14778=CIRCLE ( 'NONE', #11744, 4.000000000000000000 ) ;
#14808=ORIENTED_EDGE ( 'NONE', *, *, #11792, .T. ) ;
#14825=ADVANCED_FACE ( 'NONE', ( #5502 ), #18259, .F. ) ;
#14841=VECTOR ( 'NONE', #7729, 999.9999999999998863 ) ;
#14849=CARTESIAN_POINT ( 'NONE',  ( 4.197393957002303999, 7.772902908466098641E-14, -3.503767560748929810 ) ) ;
#14855=EDGE_LOOP ( 'NONE', ( #17252, #5546, #8493 ) ) ;
#14896=CARTESIAN_POINT ( 'NONE',  ( 1.411581201560190495E-15, 4.862606272033091592, -3.745885042887436622 ) ) ;
#14908=ORIENTED_EDGE ( 'NONE', *, *, #2432, .F. ) ;
#14909=CARTESIAN_POINT ( 'NONE',  ( -4.000000000000000000, 2.309401076758498483, -0.4999999999999927280 ) ) ;
#14932=ADVANCED_FACE ( 'NONE', ( #6647 ), #11105, .T. ) ;
#14945=CARTESIAN_POINT ( 'NONE',  ( 2.855764796983346177, -2.970025579236428737, -0.09382832055446485575 ) ) ;
#14957=B_SPLINE_CURVE_WITH_KNOTS ( 'NONE', 3,
 ( #13248, #6004, #13355, #302, #3440, #387 ),
 .UNSPECIFIED., .F., .F.,
 ( 4, 2, 4 ),
 ( 0.000000000000000000, 0.0002095117440864791795, 0.0004190234881729583589 ),
 .UNSPECIFIED. ) ;
#14971=FACE_OUTER_BOUND ( 'NONE', #13747, .T. ) ;
#14988=CARTESIAN_POINT ( 'NONE',  ( -4.000000000000000000, 2.309401076758498483, -3.433295621305379353 ) ) ;
#15000=CARTESIAN_POINT ( 'NONE',  ( -2.345747346278108214, 3.264484291692489215, -0.01223254789873409049 ) ) ;
#15007=VECTOR ( 'NONE', #8552, 1000.000000000000000 ) ;
#15008=DIRECTION ( 'NONE',  ( -1.000000000000000000, 0.000000000000000000, 0.000000000000000000 ) ) ;
#15098=ORIENTED_EDGE ( 'NONE', *, *, #10423, .F. ) ;
#15111=UNCERTAINTY_MEASURE_WITH_UNIT (LENGTH_MEASURE( 1.000000000000000082E-05 ), #16276, 'distance_accuracy_value', 'NONE');
#15115=CARTESIAN_POINT ( 'NONE',  ( 0.02448733951239481094, 4.877042772274728044, -3.751161874094022242 ) ) ;
#15149=VECTOR ( 'NONE', #5844, 1000.000000000000000 ) ;
#15196=CARTESIAN_POINT ( 'NONE',  ( -4.000000000000000000, 2.309401076758498483, -5.000000000000000000 ) ) ;
#15245=FACE_OUTER_BOUND ( 'NONE', #14469, .T. ) ;
#15285=( BOUNDED_SURFACE ( )  B_SPLINE_SURFACE ( 3, 2, ( 
 ( #13773, #440, #15115 ),
 ( #9195, #7585, #1959 ),
 ( #16536, #11962, #352 ),
 ( #13408, #6442, #544 ),
 ( #6153, #12245, #6246 ),
 ( #17769, #12054, #16254 ) ),
 .UNSPECIFIED., .F., .F., .T. ) 
 B_SPLINE_SURFACE_WITH_KNOTS ( ( 4, 2, 4 ),
 ( 3, 3 ),
 ( 0.02032853247518125531, 0.02278863295364820865, 0.02524873343211516200 ),
 ( 0.000000000000000000, 1.000000000000000000 ),
 .UNSPECIFIED. ) 
 GEOMETRIC_REPRESENTATION_ITEM ( )  RATIONAL_B_SPLINE_SURFACE ( (
 ( 1.000000000000000000, 0.8047781615896836271, 1.000000000000000000),
 ( 1.000000000000000000, 0.8123767586289967202, 1.000000000000000000),
 ( 1.000000000000000000, 0.8190662415563443322, 1.000000000000000000),
 ( 1.000000000000000000, 0.8192361015669982205, 1.000000000000000000),
 ( 1.000000000000000000, 0.8126135807103181952, 1.000000000000000000),
 ( 1.000000000000000000, 0.8047712338318587788, 1.000000000000000000) ) ) 
 REPRESENTATION_ITEM ( '' )  SURFACE ( )  );
#15296=ORIENTED_EDGE ( 'NONE', *, *, #10055, .T. ) ;
#15317=VECTOR ( 'NONE', #4336, 1000.000000000000000 ) ;
#15321=VERTEX_POINT ( 'NONE', #10899 ) ;
#15330=CARTESIAN_POINT ( 'NONE',  ( 4.000000000000000000, -0.8732470631449981147, -3.223155494240760088 ) ) ;
#15383=CARTESIAN_POINT ( 'NONE',  ( 0.3198814748697593746, 4.434118497892183264, -0.3507732604232499107 ) ) ;
#15397=CARTESIAN_POINT ( 'NONE',  ( -6.259644161404860030E-16, -4.618802153517027165, -5.000000000000000000 ) ) ;
#15425=LINE ( 'NONE', #3800, #5225 ) ;
#15432=VERTEX_POINT ( 'NONE', #2716 ) ;
#15436=DIRECTION ( 'NONE',  ( -1.000000000000000000, 0.000000000000000000, 0.000000000000000000 ) ) ;
#15451=ORIENTED_EDGE ( 'NONE', *, *, #6214, .T. ) ;
#15453=ORIENTED_EDGE ( 'NONE', *, *, #11450, .T. ) ;
#15468=DIRECTION ( 'NONE',  ( 0.000000000000000000, 0.000000000000000000, 1.000000000000000000 ) ) ;
#15480=CARTESIAN_POINT ( 'NONE',  ( 4.204015924366189871, -1.626724848190933548, -3.610627190413393084 ) ) ;
#15521=EDGE_CURVE ( 'NONE', #2269, #11877, #4411, .T. ) ;
#15529=CARTESIAN_POINT ( 'NONE',  ( -4.000000000000000000, 2.309401076758498483, -0.4999999999999927280 ) ) ;
#15548=AXIS2_PLACEMENT_3D ( 'NONE', #4268, #17128, #15876 ) ;
#15563=CARTESIAN_POINT ( 'NONE',  ( 1.567478505476134606E-15, 4.618802153517012066, -5.000000000000000000 ) ) ;
#15571=CARTESIAN_POINT ( 'NONE',  ( 4.197393957002303999, 7.772902908466098641E-14, -3.503767560748929810 ) ) ;
#15596=VERTEX_POINT ( 'NONE', #10683 ) ;
#15605=ORIENTED_EDGE ( 'NONE', *, *, #18432, .F. ) ;
#15619=LINE ( 'NONE', #7127, #18210 ) ;
#15622=EDGE_CURVE ( 'NONE', #15321, #3828, #1928, .T. ) ;
#15628=CARTESIAN_POINT ( 'NONE',  ( -0.6810597143197697489, -4.461075778259609770, -3.598441714920717516 ) ) ;
#15634=ORIENTED_EDGE ( 'NONE', *, *, #12013, .T. ) ;
#15639=CARTESIAN_POINT ( 'NONE',  ( 2.059999999999998721, 0.000000000000000000, -0.3080913168122742518 ) ) ;
#15641=CARTESIAN_POINT ( 'NONE',  ( 4.000000000000000888, 1.563622288139206118, -0.2253451193528334950 ) ) ;
#15648=CARTESIAN_POINT ( 'NONE',  ( -4.000000000000000000, 0.1981133338132459731, 2.096406544454392723E-17 ) ) ;
#15685=ORIENTED_EDGE ( 'NONE', *, *, #1330, .T. ) ;
#15699=CIRCLE ( 'NONE', #185, 4.000000000000000000 ) ;
#15711=ADVANCED_FACE ( 'NONE', ( #791 ), #6950, .F. ) ;
#15712=VERTEX_POINT ( 'NONE', #18304 ) ;
#15718=CARTESIAN_POINT ( 'NONE',  ( -3.510273485745307287, -2.827716139362669967, -3.610536846335890004 ) ) ;
#15780=ORIENTED_EDGE ( 'NONE', *, *, #5274, .F. ) ;
#15799=CARTESIAN_POINT ( 'NONE',  ( 0.6937372685066666156, -4.453844082567737672, -3.610536846335894445 ) ) ;
#15817=DIRECTION ( 'NONE',  ( -0.000000000000000000, -0.000000000000000000, 1.000000000000000000 ) ) ;
#15841=ORIENTED_EDGE ( 'NONE', *, *, #12721, .F. ) ;
#15850=ORIENTED_EDGE ( 'NONE', *, *, #3376, .F. ) ;
#15876=DIRECTION ( 'NONE',  ( -1.000000000000000000, 0.000000000000000000, 0.000000000000000000 ) ) ;
#15896=ORIENTED_EDGE ( 'NONE', *, *, #15979, .F. ) ;
#15961=STYLED_ITEM ( 'NONE', ( #2817 ), #17412 ) ;
#15979=EDGE_CURVE ( 'NONE', #7704, #15432, #14957, .T. ) ;
#15984=ADVANCED_FACE ( 'NONE', ( #15245 ), #5041, .F. ) ;
#16018=FACE_OUTER_BOUND ( 'NONE', #10285, .T. ) ;
#16059=EDGE_CURVE ( 'NONE', #1905, #12396, #14046, .T. ) ;
#16068=PRODUCT_DEFINITION_CONTEXT ( 'detailed design', #12172, 'design' ) ;
#16071=ORIENTED_EDGE ( 'NONE', *, *, #1330, .F. ) ;
#16102=VERTEX_POINT ( 'NONE', #15529 ) ;
#16122=EDGE_CURVE ( 'NONE', #15432, #12639, #16980, .T. ) ;
#16124=ADVANCED_FACE ( 'NONE', ( #18477 ), #2710, .T. ) ;
#16131=EDGE_CURVE ( 'NONE', #18131, #2367, #15619, .T. ) ;
#16150=( NAMED_UNIT ( * ) SI_UNIT ( $, .STERADIAN. ) SOLID_ANGLE_UNIT ( ) );
#16155=CARTESIAN_POINT ( 'NONE',  ( 0.5469614295415388128, -4.303013824935362663, -3.535263753543555598 ) ) ;
#16186=ORIENTED_EDGE ( 'NONE', *, *, #427, .F. ) ;
#16201=VERTEX_POINT ( 'NONE', #1422 ) ;
#16226=VECTOR ( 'NONE', #15468, 1000.000000000000000 ) ;
#16236=ORIENTED_EDGE ( 'NONE', *, *, #10055, .F. ) ;
#16254=CARTESIAN_POINT ( 'NONE',  ( -4.236525694536558362, 2.416953475386465211, -3.751298745799836354 ) ) ;
#16261=CARTESIAN_POINT ( 'NONE',  ( -4.024497503033714452, 2.323544716729487813, -3.572167766733750582 ) ) ;
#16264=ORIENTED_EDGE ( 'NONE', *, *, #3078, .T. ) ;
#16267=DIRECTION ( 'NONE',  ( -1.000000000000000000, 0.000000000000000000, 0.000000000000000000 ) ) ;
#16276=( LENGTH_UNIT ( ) NAMED_UNIT ( * ) SI_UNIT ( .MILLI., .METRE. ) );
#16288=AXIS2_PLACEMENT_3D ( 'NONE', #15397, #8167, #2911 ) ;
#16302=AXIS2_PLACEMENT_3D ( 'NONE', #11581, #12723, #5772 ) ;
#16376=CARTESIAN_POINT ( 'NONE',  ( 3.383466608491643077E-15, 4.736522675502341073, -3.681124513963742739 ) ) ;
#16394=AXIS2_PLACEMENT_3D ( 'NONE', #12949, #8567, #17342 ) ;
#16408=ORIENTED_EDGE ( 'NONE', *, *, #10391, .F. ) ;
#16457=CARTESIAN_POINT ( 'NONE',  ( 4.141042297810615835, -2.227970268150433863, -3.687027686973623819 ) ) ;
#16470=CARTESIAN_POINT ( 'NONE',  ( -1.654252653721913102, -3.663718938583024443, -0.01223254789874440342 ) ) ;
#16477=DIRECTION ( 'NONE',  ( -1.000000000000000000, 0.000000000000000000, 0.000000000000000000 ) ) ;
#16479=AXIS2_PLACEMENT_3D ( 'NONE', #121, #1454, #12892 ) ;
#16494=CARTESIAN_POINT ( 'NONE',  ( -4.197393957002303999, -7.773935952363655451E-14, -3.503767560748929810 ) ) ;
#16498=ORIENTED_EDGE ( 'NONE', *, *, #8625, .T. ) ;
#16536=CARTESIAN_POINT ( 'NONE',  ( -1.243802165048909503, 3.900692638707381921, -3.223146290109805800 ) ) ;
#16622=ORIENTED_EDGE ( 'NONE', *, *, #6025, .F. ) ;
#16627=CARTESIAN_POINT ( 'NONE',  ( 1.828356344711641102, 3.563200125723180900, -5.433716356636336675E-16 ) ) ;
#16650=CARTESIAN_POINT ( 'NONE',  ( 4.235886605889389145, 2.417314728048528760, -3.751161874094018245 ) ) ;
#16659=EDGE_LOOP ( 'NONE', ( #8727, #15780, #6519, #15850, #2731, #17458 ) ) ;
#16662=CARTESIAN_POINT ( 'NONE',  ( -4.211140560182196957, -2.431303136016552013, -3.745885042887436178 ) ) ;
#16668=ORIENTED_EDGE ( 'NONE', *, *, #8714, .F. ) ;
#16680=DIRECTION ( 'NONE',  ( 0.000000000000000000, 0.000000000000000000, -1.000000000000000000 ) ) ;
#16687=CARTESIAN_POINT ( 'NONE',  ( -4.000000000000000000, -0.7890432684750890990, -0.04868663549882315533 ) ) ;
#16723=CIRCLE ( 'NONE', #8503, 5.384454397937118664 ) ;
#16752=FACE_OUTER_BOUND ( 'NONE', #5305, .T. ) ;
#16764=B_SPLINE_CURVE_WITH_KNOTS ( 'NONE', 3,
 ( #16662, #18081, #5023, #1411, #4091, #11518 ),
 .UNSPECIFIED., .F., .F.,
 ( 4, 2, 4 ),
 ( -3.640115492409406142E-06, 0.0002066546034003385283, 0.0004169493222930864334 ),
 .UNSPECIFIED. ) ;
#16804=VECTOR ( 'NONE', #4204, 1000.000000000000000 ) ;
#16815=CARTESIAN_POINT ( 'NONE',  ( 3.999999999999999112, -1.539600717839012978, -3.300726591567080703 ) ) ;
#16823=CARTESIAN_POINT ( 'NONE',  ( 1.654252653721905331, 3.663718938583014229, -0.01223254789873410957 ) ) ;
#16834=FACE_OUTER_BOUND ( 'NONE', #6231, .T. ) ;
#16840=CARTESIAN_POINT ( 'NONE',  ( -0.1756481739660520902, 4.720212674038980261, -3.469390959564065291 ) ) ;
#16842=FACE_OUTER_BOUND ( 'NONE', #14702, .T. ) ;
#16850=ORIENTED_EDGE ( 'NONE', *, *, #17985, .F. ) ;
#16862=FACE_OUTER_BOUND ( 'NONE', #5138, .T. ) ;
#16863=PLANE ( 'NONE',  #13347 ) ;
#16865=CARTESIAN_POINT ( 'NONE',  ( 4.211140560182196957, -2.431303136016555122, -3.745885042887436622 ) ) ;
#16895=DIRECTION ( 'NONE',  ( -1.000000000000000000, 0.000000000000000000, 0.000000000000000000 ) ) ;
#16905=CARTESIAN_POINT ( 'NONE',  ( 4.000000000000000000, -1.084202172485504434E-14, -3.142992957459231906 ) ) ;
#16921=VERTEX_POINT ( 'NONE', #8019 ) ;
#16927=AXIS2_PLACEMENT_3D ( 'NONE', #5387, #2155, #7957 ) ;
#16928=AXIS2_PLACEMENT_3D ( 'NONE', #678, #1255, #5618 ) ;
#16931=CARTESIAN_POINT ( 'NONE',  ( -4.000000000000000000, -2.309401076758512694, -5.000000000000000000 ) ) ;
#16936=CARTESIAN_POINT ( 'NONE',  ( 3.472371940585993855, 2.614027278893175321, -3.320322319201766792 ) ) ;
#16954=ADVANCED_FACE ( 'NONE', ( #16018 ), #1876, .T. ) ;
#16961=CARTESIAN_POINT ( 'NONE',  ( 4.203935335434060505, 1.640780671294165272, -3.598452447879202598 ) ) ;
#16964=B_SPLINE_CURVE_WITH_KNOTS ( 'NONE', 3,
 ( #14608, #6027, #7359, #11841, #14510, #11747 ),
 .UNSPECIFIED., .F., .F.,
 ( 4, 2, 4 ),
 ( 0.000000000000000000, 0.0002095117440864783663, 0.0004190234881729567326 ),
 .UNSPECIFIED. ) ;
#16970=CARTESIAN_POINT ( 'NONE',  ( -0.5636800770129166693, -4.293361309317430319, -3.531542292955206275 ) ) ;
#16980=B_SPLINE_CURVE_WITH_KNOTS ( 'NONE', 3,
 ( #12668, #8478, #1155, #7044, #2669, #15718, #1337, #6957 ),
 .UNSPECIFIED., .F., .F.,
 ( 4, 2, 2, 4 ),
 ( 0.000000000000000000, 0.002450665683189818828, 0.003675998524784728459, 0.004901331366379638524 ),
 .UNSPECIFIED. ) ;
#16992=EDGE_CURVE ( 'NONE', #3828, #1353, #6439, .T. ) ;
#17003=ORIENTED_EDGE ( 'NONE', *, *, #16992, .T. ) ;
#17037=EDGE_LOOP ( 'NONE', ( #11837, #3550, #10081, #3528 ) ) ;
#17074=CARTESIAN_POINT ( 'NONE',  ( -1.274258131565027874, -3.883108878240886241, -3.220599429844051009 ) ) ;
#17086=CARTESIAN_POINT ( 'NONE',  ( 4.000000000000000000, 0.7924765000094659007, -0.05906175389889852662 ) ) ;
#17126=DIRECTION ( 'NONE',  ( 1.000000000000000000, 0.000000000000000000, 0.000000000000000000 ) ) ;
#17128=DIRECTION ( 'NONE',  ( -0.000000000000000000, 0.000000000000000000, -1.000000000000000000 ) ) ;
#17138=EDGE_LOOP ( 'NONE', ( #13208, #6953, #4955 ) ) ;
#17252=ORIENTED_EDGE ( 'NONE', *, *, #6549, .F. ) ;
#17262=CIRCLE ( 'NONE', #6588, 2.100000000000000089 ) ;
#17308=ORIENTED_EDGE ( 'NONE', *, *, #15622, .F. ) ;
#17342=DIRECTION ( 'NONE',  ( -1.000000000000000000, 0.000000000000000000, 0.000000000000000000 ) ) ;
#17350=CARTESIAN_POINT ( 'NONE',  ( -1.287237434361707233, -3.875615274277397937, -3.430618716626816500 ) ) ;
#17359=EDGE_CURVE ( 'NONE', #16921, #13860, #1892, .T. ) ;
#17393=( NAMED_UNIT ( * ) SI_UNIT ( $, .STERADIAN. ) SOLID_ANGLE_UNIT ( ) );
#17394=AXIS2_PLACEMENT_3D ( 'NONE', #4315, #18690, #5829 ) ;
#17412=ADVANCED_BREP_SHAPE_REPRESENTATION ( '', ( #3693, #8017 ), #6229 ) ;
#17427=CARTESIAN_POINT ( 'NONE',  ( -4.000000000000000000, 1.677772373332757194, -3.535253723897187506 ) ) ;
#17445=ORIENTED_EDGE ( 'NONE', *, *, #8982, .T. ) ;
#17451=ORIENTED_EDGE ( 'NONE', *, *, #16059, .F. ) ;
#17458=ORIENTED_EDGE ( 'NONE', *, *, #10174, .F. ) ;
#17495=CARTESIAN_POINT ( 'NONE',  ( 4.211140560182196957, -2.431303136016555122, -3.745885042887436622 ) ) ;
#17508=EDGE_CURVE ( 'NONE', #2818, #1905, #5537, .T. ) ;
#17577=ORIENTED_EDGE ( 'NONE', *, *, #17963, .F. ) ;
#17591=VERTEX_POINT ( 'NONE', #3051 ) ;
#17645=CARTESIAN_POINT ( 'NONE',  ( 0.000000000000000000, 0.000000000000000000, -5.000000000000000888 ) ) ;
#17662=CARTESIAN_POINT ( 'NONE',  ( 1.999999999999998224, -3.464101615137772594, -3.142992957459239012 ) ) ;
#17663=ORIENTED_EDGE ( 'NONE', *, *, #6249, .F. ) ;
#17675=CARTESIAN_POINT ( 'NONE',  ( 0.6640947660595348800, -4.471078309994175548, -3.602146406945708090 ) ) ;
#17678=CARTESIAN_POINT ( 'NONE',  ( -2.688821387764050996E-14, -4.618802153517012954, -0.4999999999999995559 ) ) ;
#17700=ORIENTED_EDGE ( 'NONE', *, *, #15979, .T. ) ;
#17743=CIRCLE ( 'NONE', #11057, 4.000000000000000000 ) ;
#17747=DIRECTION ( 'NONE',  ( -0.000000000000000000, -0.000000000000000000, 1.000000000000000000 ) ) ;
#17750=CARTESIAN_POINT ( 'NONE',  ( 3.510273485745307731, 2.827716139362654424, -3.610536846335885564 ) ) ;
#17752=ORIENTED_EDGE ( 'NONE', *, *, #18570, .F. ) ;
#17755=CARTESIAN_POINT ( 'NONE',  ( -2.687328764639638656, 3.067272167851286202, -0.05923475698270370959 ) ) ;
#17764=ORIENTED_EDGE ( 'NONE', *, *, #12721, .T. ) ;
#17769=CARTESIAN_POINT ( 'NONE',  ( -4.175648173966055587, 2.207990556236529844, -3.469390959564062626 ) ) ;
#17788=CARTESIAN_POINT ( 'NONE',  ( 1.411581201560190495E-15, 4.862606272033091592, -3.745885042887436622 ) ) ;
#17849=ORIENTED_EDGE ( 'NONE', *, *, #17508, .F. ) ;
#17859=VECTOR ( 'NONE', #8457, 1000.000000000000227 ) ;
#17879=DIRECTION ( 'NONE',  ( -0.8191520442889902442, 0.000000000000000000, -0.5735764363510482688 ) ) ;
#17886=ORIENTED_EDGE ( 'NONE', *, *, #13104, .F. ) ;
#17963=EDGE_CURVE ( 'NONE', #9323, #15432, #4027, .T. ) ;
#17977=CARTESIAN_POINT ( 'NONE',  ( -4.000000000000003553, 2.309401076758496263, -3.504269196027868905 ) ) ;
#17982=FACE_OUTER_BOUND ( 'NONE', #4716, .T. ) ;
#17985=EDGE_CURVE ( 'NONE', #7161, #16102, #1504, .T. ) ;
#17999=CARTESIAN_POINT ( 'NONE',  ( 4.211405965630455661, 2.460463115436283932, -3.751298928144577882 ) ) ;
#18047=CARTESIAN_POINT ( 'NONE',  ( 4.000000000000000888, 1.539600717838996990, -3.300726591567079815 ) ) ;
#18055=CARTESIAN_POINT ( 'NONE',  ( -5.560781378645575757, 6.809993116116508640E-16, -4.000000000000000000 ) ) ;
#18059=LINE ( 'NONE', #839, #18238 ) ;
#18067=ORIENTED_EDGE ( 'NONE', *, *, #15521, .F. ) ;
#18068=CARTESIAN_POINT ( 'NONE',  ( -5.384454397937118664, 6.594054843588581554E-16, -4.484454397937119197 ) ) ;
#18073=ADVANCED_FACE ( 'NONE', ( #4917 ), #15285, .F. ) ;
#18076=CARTESIAN_POINT ( 'NONE',  ( 4.197393957002303999, 7.772902908466098641E-14, -3.503767560748929810 ) ) ;
#18081=CARTESIAN_POINT ( 'NONE',  ( -4.154094228333820915, -2.398367420967594921, -3.721909803043257803 ) ) ;
#18091=CARTESIAN_POINT ( 'NONE',  ( 4.000000000000000000, 0.8378280264232961239, -3.220590601395640018 ) ) ;
#18131=VERTEX_POINT ( 'NONE', #3399 ) ;
#18167=DIRECTION ( 'NONE',  ( -1.000000000000000000, 1.224646799147352714E-16, 0.000000000000000000 ) ) ;
#18187=ORIENTED_EDGE ( 'NONE', *, *, #12014, .T. ) ;
#18206=ORIENTED_EDGE ( 'NONE', *, *, #14693, .T. ) ;
#18210=VECTOR ( 'NONE', #4097, 1000.000000000000000 ) ;
#18234=CARTESIAN_POINT ( 'NONE',  ( -1.747541505913277282, 3.837784562140256650, -3.503702292528906526 ) ) ;
#18238=VECTOR ( 'NONE', #17879, 1000.000000000000114 ) ;
#18240=CARTESIAN_POINT ( 'NONE',  ( -6.259644161404860030E-16, -4.618802153517027165, -5.000000000000000000 ) ) ;
#18251=EDGE_LOOP ( 'NONE', ( #15605, #6492, #9200, #9249, #6532 ) ) ;
#18259=CYLINDRICAL_SURFACE ( 'NONE', #1442, 2.100000000000000089 ) ;
#18264=FACE_OUTER_BOUND ( 'NONE', #3572, .T. ) ;
#18289=DIRECTION ( 'NONE',  ( 0.000000000000000000, -1.000000000000000000, 0.000000000000000000 ) ) ;
#18291=CARTESIAN_POINT ( 'NONE',  ( -3.453038570459499024, -2.625189405340453419, -3.535263753545272891 ) ) ;
#18292=CARTESIAN_POINT ( 'NONE',  ( -4.000000000000000000, -1.560351142792950618, -0.2242961665059814425 ) ) ;
#18304=CARTESIAN_POINT ( 'NONE',  ( -2.500000000000000888, 0.000000000000000000, -4.974599999999998801 ) ) ;
#18321=DIRECTION ( 'NONE',  ( -1.000000000000000000, 0.000000000000000000, 0.000000000000000000 ) ) ;
#18324=B_SPLINE_CURVE_WITH_KNOTS ( 'NONE', 3,
 ( #6625, #16815, #16905, #18047, #922 ),
 .UNSPECIFIED., .F., .F.,
 ( 4, 1, 4 ),
 ( 0.000000000000000000, 0.002309401076758505790, 0.004618802153517011580 ),
 .UNSPECIFIED. ) ;
#18359=ORIENTED_EDGE ( 'NONE', *, *, #10174, .T. ) ;
#18373=CARTESIAN_POINT ( 'NONE',  ( 4.000000000000000888, 0.8228435280416209752, -3.430609588141487976 ) ) ;
#18401=CARTESIAN_POINT ( 'NONE',  ( 0.000000000000000000, 0.000000000000000000, -25.03750572909317285 ) ) ;
#18422=EDGE_CURVE ( 'NONE', #104, #13512, #2812, .T. ) ;
#18432=EDGE_CURVE ( 'NONE', #11956, #11483, #14338, .T. ) ;
#18477=FACE_OUTER_BOUND ( 'NONE', #11867, .T. ) ;
#18488=CARTESIAN_POINT ( 'NONE',  ( 0.000000000000000000, 0.000000000000000000, 0.000000000000000000 ) ) ;
#18489=CARTESIAN_POINT ( 'NONE',  ( 4.000000000000000000, 2.309401076758497151, -3.433295621305379353 ) ) ;
#18493=B_SPLINE_CURVE_WITH_KNOTS ( 'NONE', 3,
 ( #3666, #6511, #9462, #1002, #2423, #5369 ),
 .UNSPECIFIED., .F., .F.,
 ( 4, 2, 4 ),
 ( 0.002365888236228001588, 0.003551327329835089319, 0.004736766423442177049 ),
 .UNSPECIFIED. ) ;
#18552=VERTEX_POINT ( 'NONE', #611 ) ;
#18557=DIRECTION ( 'NONE',  ( 1.000000000000000000, 0.000000000000000000, 0.000000000000000000 ) ) ;
#18570=EDGE_CURVE ( 'NONE', #10824, #2993, #9229, .T. ) ;
#18579=( BOUNDED_SURFACE ( )  B_SPLINE_SURFACE ( 3, 2, ( 
 ( #945, #6826, #16650 ),
 ( #16936, #13704, #5210 ),
 ( #9301, #2257, #5011 ),
 ( #3889, #6739, #10820 ),
 ( #3609, #9691, #8270 ),
 ( #16840, #14071, #1031 ) ),
 .UNSPECIFIED., .F., .F., .F. ) 
 B_SPLINE_SURFACE_WITH_KNOTS ( ( 4, 2, 4 ),
 ( 3, 3 ),
 ( 0.02032853247518126225, 0.02278863295364821212, 0.02524873343211516200 ),
 ( 0.000000000000000000, 1.000000000000000000 ),
 .UNSPECIFIED. ) 
 GEOMETRIC_REPRESENTATION_ITEM ( )  RATIONAL_B_SPLINE_SURFACE ( (
 ( 1.000000000000000000, 0.8047781615896835161, 1.000000000000000000),
 ( 1.000000000000000000, 0.8123767586291043008, 1.000000000000000000),
 ( 1.000000000000000000, 0.8190662415562011134, 1.000000000000000000),
 ( 1.000000000000000000, 0.8192361015671398849, 1.000000000000000000),
 ( 1.000000000000000000, 0.8126135807102121689, 1.000000000000000000),
 ( 1.000000000000000000, 0.8047712338318585568, 1.000000000000000000) ) ) 
 REPRESENTATION_ITEM ( '' )  SURFACE ( )  );
#18607=FACE_OUTER_BOUND ( 'NONE', #18251, .T. ) ;
#18630=ORIENTED_EDGE ( 'NONE', *, *, #9592, .F. ) ;
#18639=CARTESIAN_POINT ( 'NONE',  ( -1.317756351988340180, 3.857995168970202116, -0.04852650426601388955 ) ) ;
#18648=DIRECTION ( 'NONE',  ( -1.000000000000000000, 0.000000000000000000, 0.000000000000000000 ) ) ;
#18672=CARTESIAN_POINT ( 'NONE',  ( -0.5449313310646672903, -4.304185902836978883, -3.316620875263469159 ) ) ;
#18676=EDGE_CURVE ( 'NONE', #11921, #11704, #2219, .T. ) ;
#18685=ORIENTED_EDGE ( 'NONE', *, *, #13318, .F. ) ;
#18690=DIRECTION ( 'NONE',  ( 0.000000000000000000, 0.000000000000000000, -1.000000000000000000 ) ) ;
#18696=CARTESIAN_POINT ( 'NONE',  ( -6.259644161404860030E-16, -4.618802153517027165, -3.433295621305388234 ) ) ;
#18699=CARTESIAN_POINT ( 'NONE',  ( 0.000000000000000000, 0.000000000000000000, -0.2800830152838844622 ) ) ;
#18702=EDGE_CURVE ( 'NONE', #5078, #4891, #17743, .T. ) ;
#18703=ORIENTED_EDGE ( 'NONE', *, *, #2432, .T. ) ;
#18719=SURFACE_SIDE_STYLE ('',( #12917 ) ) ;
#18749=DIRECTION ( 'NONE',  ( -0.000000000000000000, 0.000000000000000000, -1.000000000000000000 ) ) ;
#18751=STYLED_ITEM('',(#18883),#3693);
#18783=ADVANCED_FACE ( 'NONE', ( #5263 ), #12598, .F. ) ;
#18795=CARTESIAN_POINT ( 'NONE',  ( -4.000000000000000000, 1.941961291383472732, -0.3515519931180205448 ) ) ;
#18877=COLOUR_RGB('Black',0.12,0.14,0.17);
#18878=FILL_AREA_STYLE_COLOUR('',#18877);
#18879=FILL_AREA_STYLE('',(#18878));
#18880=SURFACE_STYLE_FILL_AREA(#18879);
#18881=SURFACE_SIDE_STYLE('',(#18880));
#18882=SURFACE_STYLE_USAGE(.BOTH.,#18881);
#18883=PRESENTATION_STYLE_ASSIGNMENT((#18882));
ENDSEC;
END-ISO-10303-21;
